ISO-10303-21;
HEADER;
FILE_DESCRIPTION (('STEP AP203'),
    '1' );
FILE_NAME ('Part6_handleknob.step',
    '2026-10-06T15:07:10',
    ( '' ),
    ( '' ),
    'SwSTEP 2.0',
    'SolidWorks 2024',
    '' );
FILE_SCHEMA (( 'AUTOMOTIVE_DESIGN' ));
ENDSEC;

DATA;
#12=AXIS2_PLACEMENT_3D ( 'NONE', #13774, #23975, #1092 ) ;
#14=DIRECTION ( 'NONE',  ( 0.000000000000000000, 1.000000000000000000, 0.000000000000000000 ) ) ;
#59=CIRCLE ( 'NONE', #14435, 12.62979293944910353 ) ;
#65=ORIENTED_EDGE ( 'NONE', *, *, #16539, .T. ) ;
#72=VERTEX_POINT ( 'NONE', #1047 ) ;
#82=EDGE_CURVE ( 'NONE', #20879, #12815, #17217, .T. ) ;
#84=VECTOR ( 'NONE', #19365, 1000.000000000000227 ) ;
#110=DIRECTION ( 'NONE',  ( -0.000000000000000000, -1.000000000000000000, -0.000000000000000000 ) ) ;
#129=EDGE_CURVE ( 'NONE', #32786, #20668, #15618, .T. ) ;
#131=CARTESIAN_POINT ( 'NONE',  ( -35.00045521830035966, -0.01303574654798572707, 2.568038078148746184 ) ) ;
#144=AXIS2_PLACEMENT_3D ( 'NONE', #9896, #22118, #20259 ) ;
#181=CARTESIAN_POINT ( 'NONE',  ( -2.598264985223428969, 0.000000000000000000, 5.684322216989629695 ) ) ;
#184=AXIS2_PLACEMENT_3D ( 'NONE', #31855, #21799, #29506 ) ;
#185=LINE ( 'NONE', #10366, #12356 ) ;
#194=CIRCLE ( 'NONE', #7673, 0.5000000000000004441 ) ;
#196=DIRECTION ( 'NONE',  ( -0.000000000000000000, -0.000000000000000000, 1.000000000000000000 ) ) ;
#253=ORIENTED_EDGE ( 'NONE', *, *, #2293, .F. ) ;
#276=DIRECTION ( 'NONE',  ( 0.000000000000000000, -1.000000000000000000, 0.000000000000000000 ) ) ;
#331=SPHERICAL_SURFACE ( 'NONE', #5973, 0.5000000000000000000 ) ;
#357=DIRECTION ( 'NONE',  ( 0.000000000000000000, 0.000000000000000000, 1.000000000000000000 ) ) ;
#363=ORIENTED_EDGE ( 'NONE', *, *, #25190, .F. ) ;
#369=ORIENTED_EDGE ( 'NONE', *, *, #18274, .T. ) ;
#396=ADVANCED_FACE ( 'NONE', ( #26695 ), #12150, .T. ) ;
#412=CARTESIAN_POINT ( 'NONE',  ( 34.48223484310469189, 0.5174497483512505713, 2.981930256614498287 ) ) ;
#425=VERTEX_POINT ( 'NONE', #11999 ) ;
#445=CARTESIAN_POINT ( 'NONE',  ( 34.48223484310472031, 0.5000000000000000000, -2.552009564962230304 ) ) ;
#487=DIRECTION ( 'NONE',  ( 0.000000000000000000, 0.000000000000000000, 1.000000000000000000 ) ) ;
#515=DIRECTION ( 'NONE',  ( 0.000000000000000000, 1.000000000000000000, -3.469446951953611033E-15 ) ) ;
#535=AXIS2_PLACEMENT_3D ( 'NONE', #29828, #6903, #19297 ) ;
#546=LINE ( 'NONE', #10576, #3351 ) ;
#551=EDGE_CURVE ( 'NONE', #8703, #19157, #23122, .T. ) ;
#558=ADVANCED_FACE ( 'NONE', ( #15374 ), #27940, .T. ) ;
#567=ADVANCED_FACE ( 'NONE', ( #23085 ), #2862, .T. ) ;
#594=ORIENTED_EDGE ( 'NONE', *, *, #1096, .T. ) ;
#598=CARTESIAN_POINT ( 'NONE',  ( 34.48223484310472031, 0.000000000000000000, -2.552009564962230304 ) ) ;
#606=CIRCLE ( 'NONE', #12872, 7.981930256614262476 ) ;
#614=AXIS2_PLACEMENT_3D ( 'NONE', #4782, #32547, #27177 ) ;
#631=ADVANCED_FACE ( 'NONE', ( #20899 ), #8359, .T. ) ;
#673=ORIENTED_EDGE ( 'NONE', *, *, #10837, .T. ) ;
#686=CARTESIAN_POINT ( 'NONE',  ( 5.240875073191910261, 0.000000000000000000, 3.405250132838362642 ) ) ;
#744=DIRECTION ( 'NONE',  ( 0.7222222222222246524, 0.000000000000000000, -0.6916610887771492688 ) ) ;
#759=VECTOR ( 'NONE', #9903, 1000.000000000000000 ) ;
#768=FACE_OUTER_BOUND ( 'NONE', #20677, .T. ) ;
#773=VERTEX_POINT ( 'NONE', #29749 ) ;
#782=EDGE_CURVE ( 'NONE', #21865, #32461, #19232, .T. ) ;
#799=CARTESIAN_POINT ( 'NONE',  ( -34.62197427260419857, 18.00000000000000355, 0.3975189810868542395 ) ) ;
#805=DIRECTION ( 'NONE',  ( 0.000000000000000000, -1.000000000000000000, 0.000000000000000000 ) ) ;
#824=DIRECTION ( 'NONE',  ( -1.000000000000000000, 0.000000000000000000, -0.000000000000000000 ) ) ;
#842=DIRECTION ( 'NONE',  ( 0.000000000000000000, 0.000000000000000000, 1.000000000000000000 ) ) ;
#849=ORIENTED_EDGE ( 'NONE', *, *, #26141, .F. ) ;
#860=ORIENTED_EDGE ( 'NONE', *, *, #3468, .F. ) ;
#891=ORIENTED_EDGE ( 'NONE', *, *, #15986, .F. ) ;
#900=CARTESIAN_POINT ( 'NONE',  ( -34.99740252253902639, 0.5174497483512505713, 2.982117921349408007 ) ) ;
#914=ORIENTED_EDGE ( 'NONE', *, *, #129, .T. ) ;
#931=ORIENTED_EDGE ( 'NONE', *, *, #18046, .F. ) ;
#939=CARTESIAN_POINT ( 'NONE',  ( 12.44989959798868817, -0.06979899340500209104, 13.00000000000004441 ) ) ;
#949=FACE_OUTER_BOUND ( 'NONE', #14062, .T. ) ;
#961=EDGE_LOOP ( 'NONE', ( #15262, #23988, #4017, #14320 ) ) ;
#974=VERTEX_POINT ( 'NONE', #18030 ) ;
#1001=ORIENTED_EDGE ( 'NONE', *, *, #5940, .F. ) ;
#1010=ORIENTED_EDGE ( 'NONE', *, *, #29590, .T. ) ;
#1047=CARTESIAN_POINT ( 'NONE',  ( -34.31843563627105453, 19.51744974835125035, -1.818740222761503045 ) ) ;
#1054=CIRCLE ( 'NONE', #19739, 0.5000000000000003331 ) ;
#1057=CARTESIAN_POINT ( 'NONE',  ( 0.000000000000000000, 0.5174497483512452423, 0.000000000000000000 ) ) ;
#1073=CIRCLE ( 'NONE', #24010, 12.00121908859764552 ) ;
#1089=DIRECTION ( 'NONE',  ( -0.000000000000000000, -1.000000000000000000, -0.000000000000000000 ) ) ;
#1092=DIRECTION ( 'NONE',  ( 1.387778780781445676E-14, -1.000000000000000000, -9.540979117872439019E-15 ) ) ;
#1096=EDGE_CURVE ( 'NONE', #7166, #773, #22970, .T. ) ;
#1101=AXIS2_PLACEMENT_3D ( 'NONE', #31790, #3547, #23907 ) ;
#1118=EDGE_LOOP ( 'NONE', ( #5295, #20471, #21757 ) ) ;
#1152=CIRCLE ( 'NONE', #10759, 0.4999999999999996669 ) ;
#1160=DIRECTION ( 'NONE',  ( 1.000000000000000000, -0.000000000000000000, 0.000000000000000000 ) ) ;
#1166=EDGE_CURVE ( 'NONE', #27059, #7057, #19779, .T. ) ;
#1186=CIRCLE ( 'NONE', #32696, 0.5000000000000000000 ) ;
#1219=EDGE_LOOP ( 'NONE', ( #4424, #27223, #30890, #20774 ) ) ;
#1221=EDGE_CURVE ( 'NONE', #24949, #4203, #9804, .T. ) ;
#1230=CARTESIAN_POINT ( 'NONE',  ( -1.075551320669168476, 0.000000000000000000, 7.404527507138929820 ) ) ;
#1250=AXIS2_PLACEMENT_3D ( 'NONE', #22194, #22345, #9624 ) ;
#1255=AXIS2_PLACEMENT_3D ( 'NONE', #25344, #25158, #23173 ) ;
#1260=VECTOR ( 'NONE', #196, 1000.000000000000000 ) ;
#1261=CIRCLE ( 'NONE', #32770, 0.4999999999999996114 ) ;
#1289=CARTESIAN_POINT ( 'NONE',  ( 0.000000000000000000, 18.00000000000000355, -3.750000000000000444 ) ) ;
#1294=CARTESIAN_POINT ( 'NONE',  ( 32.99878091140234915, 0.000000000000000000, 0.9987809114025785195 ) ) ;
#1306=VECTOR ( 'NONE', #15568, 1000.000000000000000 ) ;
#1313=DIRECTION ( 'NONE',  ( 0.000000000000000000, 1.000000000000000000, 0.000000000000000000 ) ) ;
#1320=DIRECTION ( 'NONE',  ( 0.000000000000000000, 0.000000000000000000, 1.000000000000000000 ) ) ;
#1334=ORIENTED_EDGE ( 'NONE', *, *, #10499, .T. ) ;
#1367=ORIENTED_EDGE ( 'NONE', *, *, #3302, .F. ) ;
#1376=DIRECTION ( 'NONE',  ( -3.469446951953478110E-15, 0.000000000000000000, 1.000000000000000000 ) ) ;
#1400=ORIENTED_EDGE ( 'NONE', *, *, #13463, .F. ) ;
#1401=DIRECTION ( 'NONE',  ( -0.9896144216807899463, 0.000000000000000000, -0.1437473352845038410 ) ) ;
#1436=DIRECTION ( 'NONE',  ( 0.000000000000000000, -0.000000000000000000, 1.000000000000000000 ) ) ;
#1445=CARTESIAN_POINT ( 'NONE',  ( 0.000000000000000000, 19.50000000000000000, 0.000000000000000000 ) ) ;
#1461=ADVANCED_FACE ( 'NONE', ( #16127 ), #3461, .F. ) ;
#1468=ORIENTED_EDGE ( 'NONE', *, *, #11325, .T. ) ;
#1512=CARTESIAN_POINT ( 'NONE',  ( -33.81874022276151237, 19.50000000000000000, 1.977928362984240573 ) ) ;
#1524=DIRECTION ( 'NONE',  ( 8.678904333908113252E-16, 0.000000000000000000, -1.000000000000000000 ) ) ;
#1546=CARTESIAN_POINT ( 'NONE',  ( -34.48223484310472031, 0.5000000000000000000, 2.552009564962238297 ) ) ;
#1579=ORIENTED_EDGE ( 'NONE', *, *, #20186, .T. ) ;
#1618=CARTESIAN_POINT ( 'NONE',  ( -12.44989959798873791, 20.00000000000000000, -1.818740222761504599 ) ) ;
#1621=VECTOR ( 'NONE', #12295, 1000.000000000000114 ) ;
#1634=CARTESIAN_POINT ( 'NONE',  ( 34.48223484310469900, 0.5000000000000000000, 2.482234843104950350 ) ) ;
#1643=EDGE_LOOP ( 'NONE', ( #10456, #32959, #14875, #30341, #27670, #10174, #30850, #10845, #20092, #17328, #19615 ) ) ;
#1655=EDGE_LOOP ( 'NONE', ( #849, #17253, #24445, #22913 ) ) ;
#1688=AXIS2_PLACEMENT_3D ( 'NONE', #14919, #25128, #28145 ) ;
#1709=ORIENTED_EDGE ( 'NONE', *, *, #2626, .T. ) ;
#1733=CARTESIAN_POINT ( 'NONE',  ( 0.000000000000000000, 19.51744974835125035, 7.318435636271054534 ) ) ;
#1735=AXIS2_PLACEMENT_3D ( 'NONE', #21226, #1160, #16206 ) ;
#1736=DIRECTION ( 'NONE',  ( 0.9896144216807899463, -0.000000000000000000, 0.1437473352845038410 ) ) ;
#1744=EDGE_CURVE ( 'NONE', #23377, #9415, #27267, .T. ) ;
#1758=AXIS2_PLACEMENT_3D ( 'NONE', #7273, #2271, #12455 ) ;
#1774=CARTESIAN_POINT ( 'NONE',  ( -1.149978682276028286, 0.000000000000000000, 7.916915373446320459 ) ) ;
#1814=DIRECTION ( 'NONE',  ( 3.469446951953478110E-15, 1.087146173449926665E-32, -1.000000000000000000 ) ) ;
#1834=AXIS2_PLACEMENT_3D ( 'NONE', #1634, #11654, #6964 ) ;
#1901=ORIENTED_EDGE ( 'NONE', *, *, #24305, .T. ) ;
#1916=CARTESIAN_POINT ( 'NONE',  ( -34.48223484310472031, 0.5000000000000000000, 2.552009564962238741 ) ) ;
#1920=ORIENTED_EDGE ( 'NONE', *, *, #26984, .F. ) ;
#1922=DIRECTION ( 'NONE',  ( 1.000000000000000000, -0.000000000000000000, 0.000000000000000000 ) ) ;
#1924=ORIENTED_EDGE ( 'NONE', *, *, #4851, .T. ) ;
#1953=ORIENTED_EDGE ( 'NONE', *, *, #10639, .F. ) ;
#1958=EDGE_LOOP ( 'NONE', ( #5140, #30611, #5689, #10172 ) ) ;
#1966=CYLINDRICAL_SURFACE ( 'NONE', #614, 0.5000000000000000000 ) ;
#1976=ORIENTED_EDGE ( 'NONE', *, *, #21065, .F. ) ;
#1986=ORIENTED_EDGE ( 'NONE', *, *, #21805, .T. ) ;
#2010=ORIENTED_EDGE ( 'NONE', *, *, #7749, .F. ) ;
#2039=PLANE ( 'NONE',  #13486 ) ;
#2078=ORIENTED_EDGE ( 'NONE', *, *, #21914, .F. ) ;
#2086=DIRECTION ( 'NONE',  ( -0.03488359650710497195, -0.9989355049964838695, 0.03018263660036222401 ) ) ;
#2103=DIRECTION ( 'NONE',  ( 0.9896144216807899463, 8.678901113238557421E-19, 0.1437473352845038133 ) ) ;
#2104=DIRECTION ( 'NONE',  ( 1.000000000000000000, 0.000000000000000000, 0.000000000000000000 ) ) ;
#2143=CARTESIAN_POINT ( 'NONE',  ( 12.44989959798868817, 0.5000000000000000000, 13.00000000000004441 ) ) ;
#2169=CARTESIAN_POINT ( 'NONE',  ( -3.078042720788275233, 4.239848598108476807, 5.465019080499222248 ) ) ;
#2187=CIRCLE ( 'NONE', #3270, 0.4999999999999995559 ) ;
#2207=VECTOR ( 'NONE', #30222, 1000.000000000000000 ) ;
#2221=CARTESIAN_POINT ( 'NONE',  ( 12.44989959798868817, 0.000000000000000000, 13.00000000000004441 ) ) ;
#2271=DIRECTION ( 'NONE',  ( 1.000000000000000000, 0.000000000000000000, 0.000000000000000000 ) ) ;
#2275=ORIENTED_EDGE ( 'NONE', *, *, #24314, .T. ) ;
#2277=AXIS2_PLACEMENT_3D ( 'NONE', #13772, #1089, #32009 ) ;
#2281=AXIS2_PLACEMENT_3D ( 'NONE', #27471, #23985, #29973 ) ;
#2293=EDGE_CURVE ( 'NONE', #29995, #6237, #29872, .T. ) ;
#2313=CIRCLE ( 'NONE', #12958, 6.250000000000000000 ) ;
#2314=AXIS2_PLACEMENT_3D ( 'NONE', #2221, #7240, #4575 ) ;
#2316=LINE ( 'NONE', #9826, #27373 ) ;
#2334=AXIS2_PLACEMENT_3D ( 'NONE', #19138, #3766, #3950 ) ;
#2358=DIRECTION ( 'NONE',  ( 0.000000000000000000, -0.000000000000000000, 1.000000000000000000 ) ) ;
#2399=CARTESIAN_POINT ( 'NONE',  ( 33.81874022276150527, 19.50000000000000000, -1.977928362984233246 ) ) ;
#2428=ADVANCED_FACE ( 'NONE', ( #30377 ), #25679, .T. ) ;
#2479=PLANE ( 'NONE',  #30141 ) ;
#2508=DIRECTION ( 'NONE',  ( 0.000000000000000000, 1.000000000000000000, 0.000000000000000000 ) ) ;
#2532=EDGE_CURVE ( 'NONE', #10028, #24965, #27978, .T. ) ;
#2557=CARTESIAN_POINT ( 'NONE',  ( 34.49361350329744624, 0.1741578047003297103, 2.493613503297694933 ) ) ;
#2603=EDGE_CURVE ( 'NONE', #30805, #23785, #9593, .T. ) ;
#2620=CYLINDRICAL_SURFACE ( 'NONE', #18682, 0.5000000000000004441 ) ;
#2626=EDGE_CURVE ( 'NONE', #22752, #26914, #12264, .T. ) ;
#2637=DIRECTION ( 'NONE',  ( 0.000000000000000000, 0.000000000000000000, -1.000000000000000000 ) ) ;
#2659=FACE_OUTER_BOUND ( 'NONE', #31742, .T. ) ;
#2662=VECTOR ( 'NONE', #2103, 1000.000000000000114 ) ;
#2686=AXIS2_PLACEMENT_3D ( 'NONE', #19176, #26879, #29214 ) ;
#2714=CIRCLE ( 'NONE', #29398, 0.4999999999999996669 ) ;
#2721=DIRECTION ( 'NONE',  ( -3.469446951953478110E-15, 0.000000000000000000, 1.000000000000000000 ) ) ;
#2748=CYLINDRICAL_SURFACE ( 'NONE', #12972, 0.5000000000000004441 ) ;
#2787=ORIENTED_EDGE ( 'NONE', *, *, #26098, .F. ) ;
#2801=EDGE_CURVE ( 'NONE', #16210, #29752, #28283, .T. ) ;
#2809=LINE ( 'NONE', #799, #15531 ) ;
#2851=CONICAL_SURFACE ( 'NONE', #15637, 8.000000000000000000, 0.03490658503988666728 ) ;
#2862=TOROIDAL_SURFACE ( 'NONE', #25799, 11.18125977723849296, 0.5000000000000000000 ) ;
#2865=AXIS2_PLACEMENT_3D ( 'NONE', #14796, #7619, #2104 ) ;
#2868=CIRCLE ( 'NONE', #29990, 0.4999999999999997780 ) ;
#2869=DIRECTION ( 'NONE',  ( 0.000000000000000000, 0.000000000000000000, 1.000000000000000000 ) ) ;
#2890=CARTESIAN_POINT ( 'NONE',  ( 0.000000000000000000, 0.000000000000000000, 0.000000000000000000 ) ) ;
#2900=EDGE_CURVE ( 'NONE', #4203, #28083, #13845, .T. ) ;
#2921=LINE ( 'NONE', #30825, #15073 ) ;
#2969=DIRECTION ( 'NONE',  ( 0.1437473352845032581, 0.000000000000000000, -0.9896144216807900573 ) ) ;
#3038=MECHANICAL_CONTEXT ( 'NONE', #16282, 'mechanical' ) ;
#3099=LINE ( 'NONE', #15929, #23164 ) ;
#3115=ORIENTED_EDGE ( 'NONE', *, *, #13688, .F. ) ;
#3128=EDGE_LOOP ( 'NONE', ( #4427, #19266, #16434, #22226 ) ) ;
#3141=DIRECTION ( 'NONE',  ( 0.000000000000000000, 0.000000000000000000, -1.000000000000000000 ) ) ;
#3148=ORIENTED_EDGE ( 'NONE', *, *, #12741, .T. ) ;
#3150=CARTESIAN_POINT ( 'NONE',  ( 34.92557263839314885, 0.5000000000000000000, -2.487612133692604921 ) ) ;
#3166=CARTESIAN_POINT ( 'NONE',  ( 0.000000000000000000, 0.000000000000000000, 0.000000000000000000 ) ) ;
#3171=DIRECTION ( 'NONE',  ( -0.9896144216807906124, -6.234046928178286825E-16, -0.1437473352845001773 ) ) ;
#3182=ADVANCED_FACE ( 'NONE', ( #10549 ), #20303, .T. ) ;
#3192=ORIENTED_EDGE ( 'NONE', *, *, #25250, .F. ) ;
#3238=CARTESIAN_POINT ( 'NONE',  ( 5.175170698068133568, 0.5000000000000000000, 5.403836275575642389 ) ) ;
#3270=AXIS2_PLACEMENT_3D ( 'NONE', #9376, #27938, #4551 ) ;
#3282=ORIENTED_EDGE ( 'NONE', *, *, #10989, .F. ) ;
#3289=AXIS2_PLACEMENT_3D ( 'NONE', #15519, #25239, #2358 ) ;
#3302=EDGE_CURVE ( 'NONE', #8298, #27019, #32598, .T. ) ;
#3305=EDGE_LOOP ( 'NONE', ( #5391, #25984, #31749 ) ) ;
#3335=AXIS2_PLACEMENT_3D ( 'NONE', #1445, #32027, #9098 ) ;
#3350=CARTESIAN_POINT ( 'NONE',  ( -32.99878091140236336, 0.000000000000000000, 1.268467860057148622 ) ) ;
#3351=VECTOR ( 'NONE', #25468, 1000.000000000000227 ) ;
#3356=LINE ( 'NONE', #30791, #1260 ) ;
#3357=VERTEX_POINT ( 'NONE', #9314 ) ;
#3364=CIRCLE ( 'NONE', #2281, 0.5000000000000004441 ) ;
#3381=DIRECTION ( 'NONE',  ( -4.339452166954056922E-15, 0.000000000000000000, -1.000000000000000000 ) ) ;
#3414=EDGE_LOOP ( 'NONE', ( #27993, #12919, #18919, #26401 ) ) ;
#3421=LINE ( 'NONE', #900, #10714 ) ;
#3444=DIRECTION ( 'NONE',  ( 0.000000000000000000, 1.000000000000000000, 0.000000000000000000 ) ) ;
#3460=SHAPE_REPRESENTATION ( 'Part6_handleknob', ( #2865 ), #7102 ) ;
#3461=PLANE ( 'NONE',  #15528 ) ;
#3464=FACE_OUTER_BOUND ( 'NONE', #961, .T. ) ;
#3467=DIRECTION ( 'NONE',  ( 0.9896144216807900573, 0.000000000000000000, 0.1437473352845041463 ) ) ;
#3468=EDGE_CURVE ( 'NONE', #9954, #22307, #16021, .T. ) ;
#3486=TOROIDAL_SURFACE ( 'NONE', #30188, 7.482234843104714983, 0.5000000000000000000 ) ;
#3500=DIRECTION ( 'NONE',  ( -0.000000000000000000, -0.9993908270190956511, -0.03489949670250104552 ) ) ;
#3511=CARTESIAN_POINT ( 'NONE',  ( 0.000000000000000000, 0.000000000000000000, 0.000000000000000000 ) ) ;
#3534=CARTESIAN_POINT ( 'NONE',  ( 0.000000000000000000, 0.000000000000000000, 0.000000000000000000 ) ) ;
#3547=DIRECTION ( 'NONE',  ( 0.7222222222222220989, 0.000000000000000000, -0.6916610887771519334 ) ) ;
#3570=ORIENTED_EDGE ( 'NONE', *, *, #1166, .T. ) ;
#3589=ORIENTED_EDGE ( 'NONE', *, *, #25118, .F. ) ;
#3623=FACE_OUTER_BOUND ( 'NONE', #23258, .T. ) ;
#3729=CARTESIAN_POINT ( 'NONE',  ( 35.00000000000000000, 0.000000000000000000, -2.999999999999995559 ) ) ;
#3742=ORIENTED_EDGE ( 'NONE', *, *, #16546, .F. ) ;
#3758=FACE_OUTER_BOUND ( 'NONE', #8118, .T. ) ;
#3759=AXIS2_PLACEMENT_3D ( 'NONE', #27541, #22850, #20037 ) ;
#3766=DIRECTION ( 'NONE',  ( -8.649074885250573632E-15, 0.03489949670250105246, 0.9993908270190957621 ) ) ;
#3767=FACE_OUTER_BOUND ( 'NONE', #26766, .T. ) ;
#3777=CYLINDRICAL_SURFACE ( 'NONE', #26315, 0.4999999999999995559 ) ;
#3818=CARTESIAN_POINT ( 'NONE',  ( 34.98193025661426248, 0.5174497483512505713, -2.552009564962228527 ) ) ;
#3825=TOROIDAL_SURFACE ( 'NONE', #17676, 7.482234843104714983, 0.5000000000000000000 ) ;
#3829=AXIS2_PLACEMENT_3D ( 'NONE', #5813, #8174, #31085 ) ;
#3841=EDGE_CURVE ( 'NONE', #17909, #24949, #31321, .T. ) ;
#3842=CARTESIAN_POINT ( 'NONE',  ( 12.44989959798868817, 19.50000000000000000, 13.00000000000004441 ) ) ;
#3863=CARTESIAN_POINT ( 'NONE',  ( 12.44989959798868817, 19.50000000000000000, -1.818740222761504599 ) ) ;
#3864=ORIENTED_EDGE ( 'NONE', *, *, #22474, .F. ) ;
#3877=CARTESIAN_POINT ( 'NONE',  ( 0.000000000000000000, 19.50000000000000000, 0.000000000000000000 ) ) ;
#3921=CARTESIAN_POINT ( 'NONE',  ( 33.81874022276149816, 19.50000000000000000, 1.818740222761735525 ) ) ;
#3947=CARTESIAN_POINT ( 'NONE',  ( 15.02212703843154529, 19.50000000000000000, -4.708247362410203252 ) ) ;
#3948=DIRECTION ( 'NONE',  ( 0.000000000000000000, 0.000000000000000000, -1.000000000000000000 ) ) ;
#3950=DIRECTION ( 'NONE',  ( 0.000000000000000000, -0.9993908270190956511, 0.03489949670250104552 ) ) ;
#3989=CARTESIAN_POINT ( 'NONE',  ( 34.31843563627104032, 19.51744974835125035, 2.301584610165278377 ) ) ;
#4015=DIRECTION ( 'NONE',  ( 0.000000000000000000, 1.000000000000000000, 0.000000000000000000 ) ) ;
#4017=ORIENTED_EDGE ( 'NONE', *, *, #22195, .F. ) ;
#4018=DIRECTION ( 'NONE',  ( -0.03487826274237468965, -0.9987827659587182882, -0.03487826274237469659 ) ) ;
#4045=CARTESIAN_POINT ( 'NONE',  ( -34.48223484310472031, 0.5000000000000000000, 3.000000000000004441 ) ) ;
#4049=DIRECTION ( 'NONE',  ( -0.6916610887771488247, 0.000000000000000000, -0.7222222222222250965 ) ) ;
#4056=DIRECTION ( 'NONE',  ( -0.9993908270190957621, 0.03489949670250105246, 0.000000000000000000 ) ) ;
#4061=DIRECTION ( 'NONE',  ( -0.1437473352845080599, 0.000000000000000000, 0.9896144216807893912 ) ) ;
#4103=CARTESIAN_POINT ( 'NONE',  ( 1.052005621165114757, 19.51744974835124680, -7.242429449796464525 ) ) ;
#4106=EDGE_CURVE ( 'NONE', #28120, #29752, #2187, .T. ) ;
#4128=ORIENTED_EDGE ( 'NONE', *, *, #29590, .F. ) ;
#4203=VERTEX_POINT ( 'NONE', #29785 ) ;
#4220=DIRECTION ( 'NONE',  ( -0.9896144216807899463, -8.678901113238557421E-19, -0.1437473352845038133 ) ) ;
#4221=CARTESIAN_POINT ( 'NONE',  ( -0.9801757370192284435, 20.00000000000000000, 6.747923662139668544 ) ) ;
#4248=VERTEX_POINT ( 'NONE', #7713 ) ;
#4266=EDGE_CURVE ( 'NONE', #7057, #19157, #20897, .T. ) ;
#4270=AXIS2_PLACEMENT_3D ( 'NONE', #18114, #6958, #27371 ) ;
#4292=DIRECTION ( 'NONE',  ( -3.469446951953478110E-15, -1.087146173449926665E-32, 1.000000000000000000 ) ) ;
#4296=CIRCLE ( 'NONE', #4270, 0.5000000000000003331 ) ;
#4319=AXIS2_PLACEMENT_3D ( 'NONE', #17025, #27231, #11688 ) ;
#4340=EDGE_CURVE ( 'NONE', #6237, #14980, #25756, .T. ) ;
#4348=VECTOR ( 'NONE', #9938, 1000.000000000000000 ) ;
#4385=ADVANCED_FACE ( 'NONE', ( #21717 ), #27306, .T. ) ;
#4420=FACE_OUTER_BOUND ( 'NONE', #26443, .T. ) ;
#4424=ORIENTED_EDGE ( 'NONE', *, *, #5940, .T. ) ;
#4427=ORIENTED_EDGE ( 'NONE', *, *, #28258, .T. ) ;
#4452=CIRCLE ( 'NONE', #1250, 0.5000000000000004441 ) ;
#4459=ORIENTED_EDGE ( 'NONE', *, *, #28987, .T. ) ;
#4473=ORIENTED_EDGE ( 'NONE', *, *, #31259, .F. ) ;
#4483=ADVANCED_FACE ( 'NONE', ( #24848 ), #1966, .T. ) ;
#4531=ORIENTED_EDGE ( 'NONE', *, *, #15541, .T. ) ;
#4545=LINE ( 'NONE', #22403, #4937 ) ;
#4547=EDGE_CURVE ( 'NONE', #5967, #23561, #19294, .T. ) ;
#4551=DIRECTION ( 'NONE',  ( 0.9993908270190957621, -0.03489949670250111491, 0.000000000000000000 ) ) ;
#4571=CARTESIAN_POINT ( 'NONE',  ( 34.55410851074696410, 0.5000000000000000000, -3.046816775802624999 ) ) ;
#4572=SPHERICAL_SURFACE ( 'NONE', #15202, 0.5000000000000000000 ) ;
#4575=DIRECTION ( 'NONE',  ( 0.000000000000000000, 0.000000000000000000, 1.000000000000000000 ) ) ;
#4606=CARTESIAN_POINT ( 'NONE',  ( -35.00000000000000000, 0.5000000000000000000, -2.982234843104710986 ) ) ;
#4610=CYLINDRICAL_SURFACE ( 'NONE', #12929, 0.5000000000000004441 ) ;
#4632=EDGE_LOOP ( 'NONE', ( #27455, #14111, #31030, #21166 ) ) ;
#4678=FACE_OUTER_BOUND ( 'NONE', #28401, .T. ) ;
#4713=DIRECTION ( 'NONE',  ( 0.000000000000000000, -1.000000000000000000, 0.000000000000000000 ) ) ;
#4724=CARTESIAN_POINT ( 'NONE',  ( -34.50091246256902622, -0.01740729335041210982, -3.000607876078560388 ) ) ;
#4729=LINE ( 'NONE', #14749, #16616 ) ;
#4776=AXIS2_PLACEMENT_3D ( 'NONE', #11344, #8664, #26230 ) ;
#4782=CARTESIAN_POINT ( 'NONE',  ( 34.99999999999999289, 0.5000000000000000000, 2.482234843104954791 ) ) ;
#4796=DIRECTION ( 'NONE',  ( -0.000000000000000000, -1.000000000000000000, -0.000000000000000000 ) ) ;
#4834=CARTESIAN_POINT ( 'NONE',  ( -12.44989959798873791, 20.00000000000000000, -12.99999999999999645 ) ) ;
#4837=FACE_BOUND ( 'NONE', #26089, .T. ) ;
#4851=EDGE_CURVE ( 'NONE', #15111, #10785, #16076, .T. ) ;
#4899=ORIENTED_EDGE ( 'NONE', *, *, #4106, .T. ) ;
#4937=VECTOR ( 'NONE', #1376, 1000.000000000000000 ) ;
#4942=CARTESIAN_POINT ( 'NONE',  ( 0.000000000000000000, 0.000000000000000000, 0.000000000000000000 ) ) ;
#4990=ORIENTED_EDGE ( 'NONE', *, *, #28175, .F. ) ;
#5004=ORIENTED_EDGE ( 'NONE', *, *, #12814, .F. ) ;
#5047=ORIENTED_EDGE ( 'NONE', *, *, #30913, .T. ) ;
#5056=CARTESIAN_POINT ( 'NONE',  ( 12.44989959798868817, 18.00000000000000355, 13.00000000000004441 ) ) ;
#5076=CARTESIAN_POINT ( 'NONE',  ( -5.533288710217214579, 0.000000000000000000, -5.777777777777776791 ) ) ;
#5089=ORIENTED_EDGE ( 'NONE', *, *, #4547, .F. ) ;
#5117=DIRECTION ( 'NONE',  ( 0.03487826274237706969, -0.9987827659587180662, 0.03487826274237759705 ) ) ;
#5140=ORIENTED_EDGE ( 'NONE', *, *, #19783, .F. ) ;
#5144=DIRECTION ( 'NONE',  ( -0.000000000000000000, -1.000000000000000000, -0.000000000000000000 ) ) ;
#5207=DIRECTION ( 'NONE',  ( 0.000000000000000000, -0.000000000000000000, 1.000000000000000000 ) ) ;
#5225=CARTESIAN_POINT ( 'NONE',  ( -34.48223484310472031, 0.5000000000000000000, 3.000000000000004441 ) ) ;
#5268=CYLINDRICAL_SURFACE ( 'NONE', #6502, 0.5000000000000000000 ) ;
#5282=EDGE_LOOP ( 'NONE', ( #32963, #27442, #8426, #24929 ) ) ;
#5291=ADVANCED_FACE ( 'NONE', ( #5324 ), #331, .T. ) ;
#5295=ORIENTED_EDGE ( 'NONE', *, *, #22195, .T. ) ;
#5306=ORIENTED_EDGE ( 'NONE', *, *, #782, .T. ) ;
#5324=FACE_OUTER_BOUND ( 'NONE', #1118, .T. ) ;
#5330=DIRECTION ( 'NONE',  ( 0.000000000000000000, 1.000000000000000000, 0.000000000000000000 ) ) ;
#5368=DIRECTION ( 'NONE',  ( 0.000000000000000000, 1.000000000000000000, 0.000000000000000000 ) ) ;
#5387=CYLINDRICAL_SURFACE ( 'NONE', #11307, 0.5000000000000004441 ) ;
#5391=ORIENTED_EDGE ( 'NONE', *, *, #23131, .F. ) ;
#5393=DIRECTION ( 'NONE',  ( 0.000000000000000000, 1.000000000000000000, 0.000000000000000000 ) ) ;
#5402=ORIENTED_EDGE ( 'NONE', *, *, #20004, .F. ) ;
#5418=ORIENTED_EDGE ( 'NONE', *, *, #22819, .F. ) ;
#5441=EDGE_CURVE ( 'NONE', #23664, #24965, #24352, .T. ) ;
#5445=CARTESIAN_POINT ( 'NONE',  ( -1.075551320669168254, 0.4999999999999998890, 7.404527507138928932 ) ) ;
#5450=AXIS2_PLACEMENT_3D ( 'NONE', #29479, #11580, #24438 ) ;
#5466=CARTESIAN_POINT ( 'NONE',  ( 12.44989959798868817, 0.5174497483512729978, 13.00000000000004441 ) ) ;
#5479=DIRECTION ( 'NONE',  ( -0.9896144216807899463, 0.000000000000000000, -0.1437473352845038410 ) ) ;
#5481=EDGE_CURVE ( 'NONE', #29098, #15236, #14154, .T. ) ;
#5489=AXIS2_PLACEMENT_3D ( 'NONE', #29030, #26031, #18994 ) ;
#5494=AXIS2_PLACEMENT_3D ( 'NONE', #23076, #30630, #14868 ) ;
#5513=FACE_OUTER_BOUND ( 'NONE', #14333, .T. ) ;
#5527=ORIENTED_EDGE ( 'NONE', *, *, #22474, .T. ) ;
#5538=ORIENTED_EDGE ( 'NONE', *, *, #16499, .F. ) ;
#5545=ORIENTED_EDGE ( 'NONE', *, *, #11325, .F. ) ;
#5560=VECTOR ( 'NONE', #4292, 1000.000000000000000 ) ;
#5594=ORIENTED_EDGE ( 'NONE', *, *, #22905, .T. ) ;
#5629=VERTEX_POINT ( 'NONE', #1618 ) ;
#5671=ORIENTED_EDGE ( 'NONE', *, *, #18274, .F. ) ;
#5675=ORIENTED_EDGE ( 'NONE', *, *, #4340, .T. ) ;
#5676=ORIENTED_EDGE ( 'NONE', *, *, #20033, .F. ) ;
#5689=ORIENTED_EDGE ( 'NONE', *, *, #11618, .F. ) ;
#5735=EDGE_LOOP ( 'NONE', ( #10219, #65, #27139, #3148 ) ) ;
#5759=DIRECTION ( 'NONE',  ( -1.387778780781445676E-14, 0.000000000000000000, 1.000000000000000000 ) ) ;
#5765=DIRECTION ( 'NONE',  ( 0.000000000000000000, 0.000000000000000000, 1.000000000000000000 ) ) ;
#5794=CARTESIAN_POINT ( 'NONE',  ( 33.81874022276151237, 20.00000000000000000, -2.395703997917895123 ) ) ;
#5797=ORIENTED_EDGE ( 'NONE', *, *, #2293, .T. ) ;
#5802=ORIENTED_EDGE ( 'NONE', *, *, #5832, .F. ) ;
#5813=CARTESIAN_POINT ( 'NONE',  ( -34.71268046341646141, -0.06979899340500209104, 1.021976849372826290 ) ) ;
#5832=EDGE_CURVE ( 'NONE', #27447, #28234, #13623, .T. ) ;
#5835=DIRECTION ( 'NONE',  ( 0.000000000000000000, -1.000000000000000000, 0.000000000000000000 ) ) ;
#5846=AXIS2_PLACEMENT_3D ( 'NONE', #18821, #13929, #24152 ) ;
#5876=ADVANCED_FACE ( 'NONE', ( #11459 ), #16503, .T. ) ;
#5891=VECTOR ( 'NONE', #24240, 1000.000000000000000 ) ;
#5897=EDGE_CURVE ( 'NONE', #25215, #21865, #28838, .T. ) ;
#5908=EDGE_CURVE ( 'NONE', #25215, #12125, #15983, .T. ) ;
#5921=VECTOR ( 'NONE', #26299, 1000.000000000000227 ) ;
#5940=EDGE_CURVE ( 'NONE', #23664, #5629, #29330, .T. ) ;
#5945=LINE ( 'NONE', #23201, #12848 ) ;
#5967=VERTEX_POINT ( 'NONE', #14774 ) ;
#5973=AXIS2_PLACEMENT_3D ( 'NONE', #28220, #10504, #10834 ) ;
#5977=ORIENTED_EDGE ( 'NONE', *, *, #11976, .T. ) ;
#5980=PLANE ( 'NONE',  #3829 ) ;
#5990=EDGE_LOOP ( 'NONE', ( #32628, #24341, #12044, #26861, #16382, #14656, #27783, #26303, #10189, #21802, #29947 ) ) ;
#6030=VERTEX_POINT ( 'NONE', #4103 ) ;
#6047=CIRCLE ( 'NONE', #28466, 0.5000000000000004441 ) ;
#6075=VERTEX_POINT ( 'NONE', #27149 ) ;
#6107=EDGE_LOOP ( 'NONE', ( #3864, #30498, #15782, #13882 ) ) ;
#6129=DIRECTION ( 'NONE',  ( -0.03487826274237470353, -0.9987827659587183993, -0.03487826274237470353 ) ) ;
#6132=FACE_OUTER_BOUND ( 'NONE', #18744, .T. ) ;
#6145=ORIENTED_EDGE ( 'NONE', *, *, #21065, .T. ) ;
#6152=ORIENTED_EDGE ( 'NONE', *, *, #26707, .F. ) ;
#6173=CARTESIAN_POINT ( 'NONE',  ( 32.99635089100449648, 0.06958667959534070580, 0.9963508910047327305 ) ) ;
#6175=FACE_OUTER_BOUND ( 'NONE', #26975, .T. ) ;
#6183=DIRECTION ( 'NONE',  ( 0.000000000000000000, 0.000000000000000000, 1.000000000000000000 ) ) ;
#6195=EDGE_CURVE ( 'NONE', #4248, #15236, #23622, .T. ) ;
#6198=CARTESIAN_POINT ( 'NONE',  ( 5.175170698068133568, 0.000000000000000000, 5.403836275575642389 ) ) ;
#6219=ORIENTED_EDGE ( 'NONE', *, *, #7566, .T. ) ;
#6237=VERTEX_POINT ( 'NONE', #16265 ) ;
#6254=EDGE_LOOP ( 'NONE', ( #15012, #24088, #20645, #28431 ) ) ;
#6285=EDGE_LOOP ( 'NONE', ( #1010, #17292, #22304, #19082 ) ) ;
#6389=ORIENTED_EDGE ( 'NONE', *, *, #8164, .F. ) ;
#6411=ORIENTED_EDGE ( 'NONE', *, *, #11165, .T. ) ;
#6444=CARTESIAN_POINT ( 'NONE',  ( -3.936147556303791983, 18.00000000000000355, 4.854816414140053382 ) ) ;
#6492=VECTOR ( 'NONE', #3500, 1000.000000000000227 ) ;
#6497=EDGE_CURVE ( 'NONE', #24814, #29452, #8576, .T. ) ;
#6502=AXIS2_PLACEMENT_3D ( 'NONE', #20807, #22971, #5759 ) ;
#6508=AXIS2_PLACEMENT_3D ( 'NONE', #11302, #29528, #16634 ) ;
#6529=CARTESIAN_POINT ( 'NONE',  ( -33.81874022276151237, 19.50000000000000000, -1.818740222761504599 ) ) ;
#6542=CARTESIAN_POINT ( 'NONE',  ( 4.716257286563768858, 19.50000000000000000, 4.924645716438879717 ) ) ;
#6585=CARTESIAN_POINT ( 'NONE',  ( -35.00000000000000000, 0.5000000000000000000, -2.482234843104710986 ) ) ;
#6596=ORIENTED_EDGE ( 'NONE', *, *, #2532, .T. ) ;
#6600=ORIENTED_EDGE ( 'NONE', *, *, #29229, .T. ) ;
#6608=FACE_OUTER_BOUND ( 'NONE', #16797, .T. ) ;
#6617=CARTESIAN_POINT ( 'NONE',  ( -5.390905497009061520, 2.994789822248785871, -3.164707540391768603 ) ) ;
#6646=CARTESIAN_POINT ( 'NONE',  ( 34.98193025661426248, 0.5174497483512505713, -2.999999999999995559 ) ) ;
#6680=ADVANCED_FACE ( 'NONE', ( #9179 ), #24393, .T. ) ;
#6689=EDGE_CURVE ( 'NONE', #3357, #29995, #20860, .T. ) ;
#6756=ORIENTED_EDGE ( 'NONE', *, *, #6689, .T. ) ;
#6771=DIRECTION ( 'NONE',  ( -0.005016709653754841333, -0.9993908270190956511, 0.03453704524619621158 ) ) ;
#6785=EDGE_CURVE ( 'NONE', #773, #5629, #27265, .T. ) ;
#6786=ORIENTED_EDGE ( 'NONE', *, *, #12471, .F. ) ;
#6826=ADVANCED_FACE ( 'NONE', ( #4678 ), #14848, .T. ) ;
#6842=CARTESIAN_POINT ( 'NONE',  ( 33.00303921916322736, -0.1219419795969453463, -1.272152312594962087 ) ) ;
#6844=DIRECTION ( 'NONE',  ( 0.000000000000000000, 0.000000000000000000, 1.000000000000000000 ) ) ;
#6847=CARTESIAN_POINT ( 'NONE',  ( 32.99878091140235625, 0.000000000000000000, -1.268467860057141294 ) ) ;
#6875=ADVANCED_FACE ( 'NONE', ( #3767 ), #32016, .F. ) ;
#6886=FACE_OUTER_BOUND ( 'NONE', #25031, .T. ) ;
#6890=EDGE_CURVE ( 'NONE', #23561, #30055, #23924, .T. ) ;
#6903=DIRECTION ( 'NONE',  ( 0.9896144216807900573, 8.583536847274380671E-16, 0.1437473352845037577 ) ) ;
#6926=CARTESIAN_POINT ( 'NONE',  ( -5.834205823644825095, 18.00000000000000355, -2.241549108841658366 ) ) ;
#6958=DIRECTION ( 'NONE',  ( 0.9896144216807900573, -1.102680533460266556E-16, 0.1437473352845034802 ) ) ;
#6964=DIRECTION ( 'NONE',  ( 1.387778780781445676E-14, 0.000000000000000000, -1.000000000000000000 ) ) ;
#6971=ORIENTED_EDGE ( 'NONE', *, *, #10989, .T. ) ;
#6981=ORIENTED_EDGE ( 'NONE', *, *, #1744, .F. ) ;
#7028=CARTESIAN_POINT ( 'NONE',  ( 0.000000000000000000, 19.50000000000000000, 0.000000000000000000 ) ) ;
#7029=( LENGTH_UNIT ( ) NAMED_UNIT ( * ) SI_UNIT ( .MILLI., .METRE. ) );
#7030=VECTOR ( 'NONE', #2721, 1000.000000000000000 ) ;
#7050=ORIENTED_EDGE ( 'NONE', *, *, #1744, .T. ) ;
#7057=VERTEX_POINT ( 'NONE', #1289 ) ;
#7073=CLOSED_SHELL ( 'NONE', ( #28326, #18885, #32916, #8247, #28388, #8330, #7790, #11076, #6680, #8150, #21838, #18049, #6875, #17947, #396, #631, #12147, #27412, #8862, #7631, #30758, #32373, #30820, #12768, #22754, #5876, #11722, #7548, #31460, #14262, #1461, #24447, #14483, #10796, #23327, #24257, #17525, #31274, #31513, #32275, #25989, #4385, #22427, #28189, #26720, #17540, #16723, #6826, #567, #32500, #10097, #3182, #558, #10226, #17170, #32207, #4483, #12440, #20586, #10755, #24076, #13608, #5291, #16514, #2428, #29476, #32929, #23517, #13579, #8678 ) ) ;
#7077=ORIENTED_EDGE ( 'NONE', *, *, #15541, .F. ) ;
#7078=CONICAL_SURFACE ( 'NONE', #14001, 8.000000000000000000, 0.03490658503988666728 ) ;
#7082=CARTESIAN_POINT ( 'NONE',  ( -32.37020706055090358, 18.00000000000000355, 0.7246014581832563861 ) ) ;
#7102=( GEOMETRIC_REPRESENTATION_CONTEXT ( 3 ) GLOBAL_UNCERTAINTY_ASSIGNED_CONTEXT ( ( #25882 ) ) GLOBAL_UNIT_ASSIGNED_CONTEXT ( ( #7029, #25074, #11267 ) ) REPRESENTATION_CONTEXT ( 'NONE', 'WORKASPACE' ) );
#7109=CARTESIAN_POINT ( 'NONE',  ( -34.48223484310472031, 0.5000000000000000000, 2.552009564962238741 ) ) ;
#7118=AXIS2_PLACEMENT_3D ( 'NONE', #27668, #20012, #25496 ) ;
#7124=EDGE_CURVE ( 'NONE', #8068, #13727, #21662, .T. ) ;
#7141=VECTOR ( 'NONE', #15431, 1000.000000000000227 ) ;
#7166=VERTEX_POINT ( 'NONE', #11969 ) ;
#7179=EDGE_CURVE ( 'NONE', #17909, #29021, #27659, .T. ) ;
#7195=FACE_OUTER_BOUND ( 'NONE', #1643, .T. ) ;
#7240=DIRECTION ( 'NONE',  ( 0.000000000000000000, 1.000000000000000000, 0.000000000000000000 ) ) ;
#7273=CARTESIAN_POINT ( 'NONE',  ( -12.44989959798873791, 0.5000000000000000000, -2.482234843104710986 ) ) ;
#7278=EDGE_CURVE ( 'NONE', #23785, #20668, #13381, .T. ) ;
#7313=EDGE_CURVE ( 'NONE', #16210, #24347, #12270, .T. ) ;
#7321=DIRECTION ( 'NONE',  ( 0.000000000000000000, 0.000000000000000000, 1.000000000000000000 ) ) ;
#7361=EDGE_CURVE ( 'NONE', #27059, #8703, #28316, .T. ) ;
#7369=ORIENTED_EDGE ( 'NONE', *, *, #2900, .T. ) ;
#7426=ORIENTED_EDGE ( 'NONE', *, *, #7179, .T. ) ;
#7428=FACE_OUTER_BOUND ( 'NONE', #10074, .T. ) ;
#7432=LINE ( 'NONE', #9608, #19931 ) ;
#7436=CARTESIAN_POINT ( 'NONE',  ( -12.44989959798873791, 0.000000000000000000, -2.482234843104710986 ) ) ;
#7455=DIRECTION ( 'NONE',  ( 0.000000000000000000, -0.000000000000000000, 1.000000000000000000 ) ) ;
#7544=EDGE_CURVE ( 'NONE', #30805, #11692, #9238, .T. ) ;
#7546=DIRECTION ( 'NONE',  ( -0.000000000000000000, -1.000000000000000000, -0.000000000000000000 ) ) ;
#7548=ADVANCED_FACE ( 'NONE', ( #9552 ), #24947, .F. ) ;
#7558=DIRECTION ( 'NONE',  ( -0.02413862388702650921, -0.9993908270190956511, -0.02520519206291740172 ) ) ;
#7559=AXIS2_PLACEMENT_3D ( 'NONE', #20120, #20769, #9907 ) ;
#7561=DIRECTION ( 'NONE',  ( 0.000000000000000000, 0.000000000000000000, 1.000000000000000000 ) ) ;
#7566=EDGE_CURVE ( 'NONE', #23561, #27019, #4729, .T. ) ;
#7589=AXIS2_PLACEMENT_3D ( 'NONE', #7028, #19741, #29781 ) ;
#7595=CARTESIAN_POINT ( 'NONE',  ( -0.9801757370192266672, 20.00000000000000000, 6.747923662139668544 ) ) ;
#7619=DIRECTION ( 'NONE',  ( 0.000000000000000000, 0.000000000000000000, 1.000000000000000000 ) ) ;
#7620=AXIS2_PLACEMENT_3D ( 'NONE', #18738, #28941, #16242 ) ;
#7631=ADVANCED_FACE ( 'NONE', ( #6886 ), #14591, .T. ) ;
#7632=VERTEX_POINT ( 'NONE', #19462 ) ;
#7644=VECTOR ( 'NONE', #27053, 1000.000000000000227 ) ;
#7651=CIRCLE ( 'NONE', #30632, 0.5000000000000000000 ) ;
#7673=AXIS2_PLACEMENT_3D ( 'NONE', #3921, #19618, #31990 ) ;
#7697=AXIS2_PLACEMENT_3D ( 'NONE', #15817, #11118, #8447 ) ;
#7713=CARTESIAN_POINT ( 'NONE',  ( -32.37020706055090358, 18.00000000000000355, -0.3702070605508915868 ) ) ;
#7723=ORIENTED_EDGE ( 'NONE', *, *, #7179, .F. ) ;
#7746=CIRCLE ( 'NONE', #13083, 11.18125977723849296 ) ;
#7749=EDGE_CURVE ( 'NONE', #26914, #11692, #17176, .T. ) ;
#7758=EDGE_CURVE ( 'NONE', #20668, #10785, #22930, .T. ) ;
#7790=ADVANCED_FACE ( 'NONE', ( #28126 ), #5387, .T. ) ;
#7886=EDGE_LOOP ( 'NONE', ( #10551, #8730, #22842, #19925 ) ) ;
#7895=DIRECTION ( 'NONE',  ( -0.000000000000000000, -1.000000000000000000, -0.000000000000000000 ) ) ;
#7915=DIRECTION ( 'NONE',  ( 0.1437473352845045071, 0.000000000000000000, -0.9896144216807898353 ) ) ;
#7997=CIRCLE ( 'NONE', #22405, 0.5000000000000003331 ) ;
#8015=SPHERICAL_SURFACE ( 'NONE', #1735, 0.5000000000000000000 ) ;
#8022=DIRECTION ( 'NONE',  ( 0.9993908270190957621, 0.03489949670250105246, 3.467333458611667963E-15 ) ) ;
#8047=VECTOR ( 'NONE', #27770, 1000.000000000000000 ) ;
#8058=VECTOR ( 'NONE', #21602, 1000.000000000000000 ) ;
#8068=VERTEX_POINT ( 'NONE', #1294 ) ;
#8108=ORIENTED_EDGE ( 'NONE', *, *, #21355, .T. ) ;
#8117=AXIS2_PLACEMENT_3D ( 'NONE', #22530, #33058, #2637 ) ;
#8118=EDGE_LOOP ( 'NONE', ( #4128, #26930 ) ) ;
#8146=EDGE_CURVE ( 'NONE', #29452, #7632, #10262, .T. ) ;
#8150=ADVANCED_FACE ( 'NONE', ( #6132 ), #23595, .T. ) ;
#8157=CARTESIAN_POINT ( 'NONE',  ( -12.44989959798873791, 0.5000000000000000000, -12.99999999999999645 ) ) ;
#8164=EDGE_CURVE ( 'NONE', #27019, #8068, #19657, .T. ) ;
#8165=CARTESIAN_POINT ( 'NONE',  ( -4.716257286563782181, 19.50000000000000000, -4.924645716438866394 ) ) ;
#8174=DIRECTION ( 'NONE',  ( -0.1436597682917712671, 0.03489949670250103858, 0.9890115753135888532 ) ) ;
#8188=CARTESIAN_POINT ( 'NONE',  ( 12.44989959798868817, 19.51744974835125035, 13.00000000000004441 ) ) ;
#8191=CARTESIAN_POINT ( 'NONE',  ( 4.592425496802574958E-16, 18.00000000000000355, 3.750000000000000444 ) ) ;
#8203=AXIS2_PLACEMENT_3D ( 'NONE', #23725, #3171, #28730 ) ;
#8204=ORIENTED_EDGE ( 'NONE', *, *, #12741, .F. ) ;
#8210=ORIENTED_EDGE ( 'NONE', *, *, #5832, .T. ) ;
#8212=ORIENTED_EDGE ( 'NONE', *, *, #30913, .F. ) ;
#8213=CARTESIAN_POINT ( 'NONE',  ( 5.390905497009046421, 2.994789822248789868, 3.164707540391793028 ) ) ;
#8224=DIRECTION ( 'NONE',  ( -1.000000000000000000, 0.000000000000000000, 0.000000000000000000 ) ) ;
#8230=EDGE_LOOP ( 'NONE', ( #369, #20549, #13640, #931 ) ) ;
#8238=CARTESIAN_POINT ( 'NONE',  ( 34.30158461016502258, 20.00000000000000000, 1.818740222761740633 ) ) ;
#8247=ADVANCED_FACE ( 'NONE', ( #32876 ), #4610, .T. ) ;
#8257=ORIENTED_EDGE ( 'NONE', *, *, #23198, .F. ) ;
#8284=DIRECTION ( 'NONE',  ( 0.000000000000000000, 1.000000000000000000, 0.000000000000000000 ) ) ;
#8291=ORIENTED_EDGE ( 'NONE', *, *, #8828, .T. ) ;
#8298=VERTEX_POINT ( 'NONE', #11973 ) ;
#8321=( BOUNDED_CURVE ( )  B_SPLINE_CURVE ( 3, ( #181, #2169, #12354, #6444 ),
 .UNSPECIFIED., .F., .F. ) 
 B_SPLINE_CURVE_WITH_KNOTS ( ( 4, 4 ),
 ( 0.2844899013887129402, 0.5370275574894024517 ),
 .UNSPECIFIED. ) 
 CURVE ( )  GEOMETRIC_REPRESENTATION_ITEM ( )  RATIONAL_B_SPLINE_CURVE ( ( 1.000000000000000000, 0.9946924518608444288, 0.9946924518608444288, 1.000000000000000000 ) ) 
 REPRESENTATION_ITEM ( '' )  );
#8330=ADVANCED_FACE ( 'NONE', ( #12618 ), #5268, .T. ) ;
#8333=DIRECTION ( 'NONE',  ( 0.000000000000000000, 0.000000000000000000, 1.000000000000000000 ) ) ;
#8359=PLANE ( 'NONE',  #18374 ) ;
#8396=VERTEX_POINT ( 'NONE', #24297 ) ;
#8422=VERTEX_POINT ( 'NONE', #31679 ) ;
#8426=ORIENTED_EDGE ( 'NONE', *, *, #27178, .T. ) ;
#8447=DIRECTION ( 'NONE',  ( 0.000000000000000000, 0.000000000000000000, -1.000000000000000000 ) ) ;
#8483=DIRECTION ( 'NONE',  ( 6.938893903907228378E-15, 0.000000000000000000, -1.000000000000000000 ) ) ;
#8508=DIRECTION ( 'NONE',  ( -0.03489949670250104552, 0.9993908270190956511, 0.000000000000000000 ) ) ;
#8529=DIRECTION ( 'NONE',  ( 0.000000000000000000, 0.000000000000000000, 1.000000000000000000 ) ) ;
#8533=DIRECTION ( 'NONE',  ( 0.02413862388702639472, -0.9993908270190956511, 0.02520519206291751621 ) ) ;
#8544=CARTESIAN_POINT ( 'NONE',  ( 35.00000000000000000, 18.00000000000000355, 0.3702070605511352808 ) ) ;
#8570=CARTESIAN_POINT ( 'NONE',  ( 0.000000000000000000, 0.5000000000000000000, 0.000000000000000000 ) ) ;
#8576=CIRCLE ( 'NONE', #23521, 0.5000000000000004441 ) ;
#8583=CONICAL_SURFACE ( 'NONE', #31557, 11.99878165403819352, 0.03490658503988666728 ) ;
#8592=CARTESIAN_POINT ( 'NONE',  ( 35.00045521830035966, -0.01303574654798581554, -2.568038078148735526 ) ) ;
#8602=DIRECTION ( 'NONE',  ( 0.000000000000000000, 1.000000000000000000, 0.000000000000000000 ) ) ;
#8604=CARTESIAN_POINT ( 'NONE',  ( 1.075551320669168476, 0.5000000000000000000, -7.404527507138929820 ) ) ;
#8621=DIRECTION ( 'NONE',  ( 0.000000000000000000, 0.000000000000000000, 1.000000000000000000 ) ) ;
#8649=CARTESIAN_POINT ( 'NONE',  ( 0.000000000000000000, 37.67766952966368876, 0.000000000000000000 ) ) ;
#8654=DIRECTION ( 'NONE',  ( 0.000000000000000000, -1.000000000000000000, 0.000000000000000000 ) ) ;
#8655=CARTESIAN_POINT ( 'NONE',  ( 2.598264985223430301, 0.000000000000000000, -5.684322216989628807 ) ) ;
#8657=EDGE_LOOP ( 'NONE', ( #23439, #15006, #891, #28063 ) ) ;
#8659=VECTOR ( 'NONE', #18013, 1000.000000000000227 ) ;
#8664=DIRECTION ( 'NONE',  ( 0.000000000000000000, 1.000000000000000000, 0.000000000000000000 ) ) ;
#8674=LINE ( 'NONE', #6173, #12462 ) ;
#8678=ADVANCED_FACE ( 'NONE', ( #14902 ), #32497, .T. ) ;
#8679=AXIS2_PLACEMENT_3D ( 'NONE', #16029, #31132, #10541 ) ;
#8703=VERTEX_POINT ( 'NONE', #25108 ) ;
#8716=DIRECTION ( 'NONE',  ( -1.000000000000000000, 0.000000000000000000, 1.388624693425302853E-14 ) ) ;
#8720=ORIENTED_EDGE ( 'NONE', *, *, #25914, .T. ) ;
#8730=ORIENTED_EDGE ( 'NONE', *, *, #2801, .T. ) ;
#8736=VERTEX_POINT ( 'NONE', #28130 ) ;
#8784=CYLINDRICAL_SURFACE ( 'NONE', #17231, 0.5000000000000004441 ) ;
#8828=EDGE_CURVE ( 'NONE', #12125, #9954, #17234, .T. ) ;
#8849=ORIENTED_EDGE ( 'NONE', *, *, #7544, .T. ) ;
#8862=ADVANCED_FACE ( 'NONE', ( #12583 ), #14546, .F. ) ;
#8890=ORIENTED_EDGE ( 'NONE', *, *, #21763, .T. ) ;
#8903=ORIENTED_EDGE ( 'NONE', *, *, #11976, .F. ) ;
#8906=CARTESIAN_POINT ( 'NONE',  ( -12.44989959798873791, 18.00000000000000355, -0.3702070605508915868 ) ) ;
#8919=VERTEX_POINT ( 'NONE', #28948 ) ;
#8969=DIRECTION ( 'NONE',  ( -0.000000000000000000, -1.000000000000000000, -0.000000000000000000 ) ) ;
#9008=DIRECTION ( 'NONE',  ( 0.000000000000000000, 0.000000000000000000, 1.000000000000000000 ) ) ;
#9078=DIRECTION ( 'NONE',  ( 0.000000000000000000, -0.000000000000000000, 1.000000000000000000 ) ) ;
#9093=CARTESIAN_POINT ( 'NONE',  ( -5.509727295071408903, 5.993169562190665545, -2.952988490976575786 ) ) ;
#9098=DIRECTION ( 'NONE',  ( 0.000000000000000000, 0.000000000000000000, 1.000000000000000000 ) ) ;
#9164=AXIS2_PLACEMENT_3D ( 'NONE', #9556, #1736, #19774 ) ;
#9179=FACE_OUTER_BOUND ( 'NONE', #19056, .T. ) ;
#9182=TOROIDAL_SURFACE ( 'NONE', #26293, 10.51776515689528502, 0.5000000000000000000 ) ;
#9195=AXIS2_PLACEMENT_3D ( 'NONE', #31157, #18256, #15083 ) ;
#9197=VECTOR ( 'NONE', #12578, 1000.000000000000000 ) ;
#9202=ORIENTED_EDGE ( 'NONE', *, *, #27178, .F. ) ;
#9204=AXIS2_PLACEMENT_3D ( 'NONE', #1916, #12089, #9555 ) ;
#9238=LINE ( 'NONE', #25103, #12899 ) ;
#9245=VERTEX_POINT ( 'NONE', #16203 ) ;
#9246=AXIS2_PLACEMENT_3D ( 'NONE', #31044, #13287, #31863 ) ;
#9275=CARTESIAN_POINT ( 'NONE',  ( 0.000000000000000000, 37.67766952966368876, 0.000000000000000000 ) ) ;
#9277=AXIS2_PLACEMENT_3D ( 'NONE', #6585, #1922, #22138 ) ;
#9282=PLANE ( 'NONE',  #6508 ) ;
#9314=CARTESIAN_POINT ( 'NONE',  ( 33.89057010690738991, 19.51744974835125035, -2.472434150641027895 ) ) ;
#9376=CARTESIAN_POINT ( 'NONE',  ( -34.48223484310472031, 0.5000000000000000000, -2.482234843104711430 ) ) ;
#9377=VERTEX_POINT ( 'NONE', #13521 ) ;
#9405=CARTESIAN_POINT ( 'NONE',  ( -33.89057010690739702, 19.51744974835125035, 2.472434150641035444 ) ) ;
#9415=VERTEX_POINT ( 'NONE', #21863 ) ;
#9421=EDGE_CURVE ( 'NONE', #14956, #20879, #16857, .T. ) ;
#9422=ORIENTED_EDGE ( 'NONE', *, *, #15212, .F. ) ;
#9434=CARTESIAN_POINT ( 'NONE',  ( 34.48223484310472031, 0.5000000000000000000, -2.552009564962230304 ) ) ;
#9436=CARTESIAN_POINT ( 'NONE',  ( 12.44989959798877877, 0.000000000000000000, 2.482234843104759392 ) ) ;
#9505=DIRECTION ( 'NONE',  ( -0.9993908270190956511, -0.03489949670250350189, 1.734723475976808475E-15 ) ) ;
#9507=SPHERICAL_SURFACE ( 'NONE', #31178, 0.5000000000000000000 ) ;
#9510=EDGE_LOOP ( 'NONE', ( #23887, #32510, #21007, #2010, #16606, #5004 ) ) ;
#9552=FACE_OUTER_BOUND ( 'NONE', #6254, .T. ) ;
#9555=DIRECTION ( 'NONE',  ( -0.1437473352844943209, 0.000000000000000000, 0.9896144216807913896 ) ) ;
#9556=CARTESIAN_POINT ( 'NONE',  ( 34.92557263839314885, 0.5000000000000000000, -2.487612133692604921 ) ) ;
#9559=VECTOR ( 'NONE', #24102, 1000.000000000000114 ) ;
#9571=EDGE_LOOP ( 'NONE', ( #594, #23018, #5676, #8204 ) ) ;
#9593=CIRCLE ( 'NONE', #20834, 0.4999999999999996669 ) ;
#9608=CARTESIAN_POINT ( 'NONE',  ( 34.99999999999998579, 0.5000000000000000000, 2.982234843104954791 ) ) ;
#9624=DIRECTION ( 'NONE',  ( 0.000000000000000000, 0.000000000000000000, 1.000000000000000000 ) ) ;
#9626=EDGE_CURVE ( 'NONE', #29952, #29340, #13495, .T. ) ;
#9641=ORIENTED_EDGE ( 'NONE', *, *, #12471, .T. ) ;
#9644=EDGE_CURVE ( 'NONE', #27615, #29098, #18848, .T. ) ;
#9665=EDGE_LOOP ( 'NONE', ( #15201, #5538, #7077, #3115 ) ) ;
#9685=DIRECTION ( 'NONE',  ( -0.000000000000000000, -1.000000000000000000, -0.000000000000000000 ) ) ;
#9707=VECTOR ( 'NONE', #31236, 1000.000000000000000 ) ;
#9737=ORIENTED_EDGE ( 'NONE', *, *, #7124, .T. ) ;
#9786=EDGE_LOOP ( 'NONE', ( #10077, #6971, #7426, #29283 ) ) ;
#9804=LINE ( 'NONE', #25001, #1621 ) ;
#9822=DIRECTION ( 'NONE',  ( 0.000000000000000000, 0.000000000000000000, -1.000000000000000000 ) ) ;
#9826=CARTESIAN_POINT ( 'NONE',  ( -32.37020706055090358, 18.00000000000000355, 3.000000000000004441 ) ) ;
#9846=EDGE_CURVE ( 'NONE', #32461, #12125, #7432, .T. ) ;
#9865=ORIENTED_EDGE ( 'NONE', *, *, #14649, .F. ) ;
#9878=CARTESIAN_POINT ( 'NONE',  ( 34.48223484310469189, 0.5000000000000000000, 2.982234843104950350 ) ) ;
#9890=CARTESIAN_POINT ( 'NONE',  ( -34.92557263839314885, 0.5000000000000000000, 2.487612133692613359 ) ) ;
#9896=CARTESIAN_POINT ( 'NONE',  ( 34.48223484310472031, 0.5000000000000000000, -2.552009564962230304 ) ) ;
#9903=DIRECTION ( 'NONE',  ( 0.03487826274237469659, 0.9987827659587182882, 0.03487826274237468965 ) ) ;
#9907=DIRECTION ( 'NONE',  ( 0.1437473352845043406, 0.000000000000000000, -0.9896144216807899463 ) ) ;
#9938=DIRECTION ( 'NONE',  ( 1.000000000000000000, -0.000000000000000000, 0.000000000000000000 ) ) ;
#9954=VERTEX_POINT ( 'NONE', #10066 ) ;
#9976=DIRECTION ( 'NONE',  ( -0.03488359650710735893, -0.9989355049964836475, 0.03018263660036427792 ) ) ;
#9977=CARTESIAN_POINT ( 'NONE',  ( 0.000000000000000000, 0.000000000000000000, 0.000000000000000000 ) ) ;
#10028=VERTEX_POINT ( 'NONE', #10240 ) ;
#10042=FACE_OUTER_BOUND ( 'NONE', #31693, .T. ) ;
#10050=LINE ( 'NONE', #15241, #8047 ) ;
#10066=CARTESIAN_POINT ( 'NONE',  ( 12.44989959798878054, 0.000000000000000000, 2.482234843104759392 ) ) ;
#10074=EDGE_LOOP ( 'NONE', ( #18884, #21558, #17332, #19039 ) ) ;
#10077=ORIENTED_EDGE ( 'NONE', *, *, #23193, .F. ) ;
#10097=ADVANCED_FACE ( 'NONE', ( #11218 ), #24263, .T. ) ;
#10133=ORIENTED_EDGE ( 'NONE', *, *, #33071, .F. ) ;
#10153=CIRCLE ( 'NONE', #2686, 0.5000000000000000000 ) ;
#10164=AXIS2_PLACEMENT_3D ( 'NONE', #17927, #8969, #19684 ) ;
#10172=ORIENTED_EDGE ( 'NONE', *, *, #31622, .T. ) ;
#10174=ORIENTED_EDGE ( 'NONE', *, *, #3468, .T. ) ;
#10189=ORIENTED_EDGE ( 'NONE', *, *, #8146, .T. ) ;
#10194=CARTESIAN_POINT ( 'NONE',  ( 0.000000000000000000, 37.67766952966368876, -3.750000000000000444 ) ) ;
#10197=DIRECTION ( 'NONE',  ( 0.000000000000000000, 0.000000000000000000, 1.000000000000000000 ) ) ;
#10211=ORIENTED_EDGE ( 'NONE', *, *, #26098, .T. ) ;
#10219=ORIENTED_EDGE ( 'NONE', *, *, #30660, .T. ) ;
#10221=CYLINDRICAL_SURFACE ( 'NONE', #26895, 0.5000000000000000000 ) ;
#10226=ADVANCED_FACE ( 'NONE', ( #19433 ), #21992, .T. ) ;
#10231=CARTESIAN_POINT ( 'NONE',  ( 0.000000000000000000, 0.000000000000000000, 0.000000000000000000 ) ) ;
#10240=CARTESIAN_POINT ( 'NONE',  ( -5.520790571833112281, 0.5174497483512503493, -5.764727407554744332 ) ) ;
#10257=DIRECTION ( 'NONE',  ( 0.1436597682917715446, 0.03489949670250103858, -0.9890115753135888532 ) ) ;
#10259=ORIENTED_EDGE ( 'NONE', *, *, #7361, .F. ) ;
#10262=CIRCLE ( 'NONE', #29473, 6.818740222761507042 ) ;
#10272=CARTESIAN_POINT ( 'NONE',  ( 34.48223484310472031, 0.5000000000000000000, -2.552009564962229859 ) ) ;
#10290=DIRECTION ( 'NONE',  ( -1.000000000000000000, 0.000000000000000000, -8.654346879536960414E-15 ) ) ;
#10299=DIRECTION ( 'NONE',  ( 0.000000000000000000, 0.000000000000000000, 1.000000000000000000 ) ) ;
#10366=CARTESIAN_POINT ( 'NONE',  ( -34.30158461016502969, 20.00000000000000000, -1.818740222761504599 ) ) ;
#10380=ORIENTED_EDGE ( 'NONE', *, *, #15628, .F. ) ;
#10419=CYLINDRICAL_SURFACE ( 'NONE', #24616, 0.4999999999999995559 ) ;
#10456=ORIENTED_EDGE ( 'NONE', *, *, #9626, .T. ) ;
#10457=DIRECTION ( 'NONE',  ( 0.9896144216807900573, -1.102680533460266556E-16, 0.1437473352845034802 ) ) ;
#10495=CYLINDRICAL_SURFACE ( 'NONE', #27885, 0.5000000000000002220 ) ;
#10499=EDGE_CURVE ( 'NONE', #4248, #29383, #2316, .T. ) ;
#10504=DIRECTION ( 'NONE',  ( 0.000000000000000000, -0.000000000000000000, 1.000000000000000000 ) ) ;
#10507=CARTESIAN_POINT ( 'NONE',  ( -12.44989959798873791, -0.06979899340500209104, -12.99999999999999645 ) ) ;
#10541=DIRECTION ( 'NONE',  ( 0.000000000000000000, 0.000000000000000000, -1.000000000000000000 ) ) ;
#10549=FACE_OUTER_BOUND ( 'NONE', #1958, .T. ) ;
#10551=ORIENTED_EDGE ( 'NONE', *, *, #7313, .F. ) ;
#10558=CARTESIAN_POINT ( 'NONE',  ( 5.533288710217197703, 0.000000000000000000, 5.777777777777793666 ) ) ;
#10576=CARTESIAN_POINT ( 'NONE',  ( 34.99744630603539974, 0.5000000000000000000, -2.982419344532999617 ) ) ;
#10595=DIRECTION ( 'NONE',  ( 1.000000000000000000, 0.000000000000000000, 0.000000000000000000 ) ) ;
#10601=EDGE_CURVE ( 'NONE', #28083, #8736, #25527, .T. ) ;
#10639=EDGE_CURVE ( 'NONE', #17664, #14956, #22554, .T. ) ;
#10666=AXIS2_PLACEMENT_3D ( 'NONE', #6542, #26946, #4049 ) ;
#10676=DIRECTION ( 'NONE',  ( 0.000000000000000000, 0.000000000000000000, -1.000000000000000000 ) ) ;
#10714=VECTOR ( 'NONE', #10746, 1000.000000000000227 ) ;
#10720=VECTOR ( 'NONE', #5835, 1000.000000000000000 ) ;
#10721=DIRECTION ( 'NONE',  ( -3.552713678800500929E-15, 0.000000000000000000, 1.000000000000000000 ) ) ;
#10727=CARTESIAN_POINT ( 'NONE',  ( -0.9801757370192284435, 19.50000000000000000, 6.747923662139668544 ) ) ;
#10746=DIRECTION ( 'NONE',  ( 0.9896144216807899463, -8.678901113238559347E-19, 0.1437473352845035635 ) ) ;
#10755=ADVANCED_FACE ( 'NONE', ( #3464 ), #8784, .T. ) ;
#10759=AXIS2_PLACEMENT_3D ( 'NONE', #7109, #22665, #30515 ) ;
#10771=VECTOR ( 'NONE', #824, 1000.000000000000000 ) ;
#10773=CARTESIAN_POINT ( 'NONE',  ( -12.44989959798873791, 0.5000000000000000000, -12.99999999999999645 ) ) ;
#10785=VERTEX_POINT ( 'NONE', #32367 ) ;
#10796=ADVANCED_FACE ( 'NONE', ( #10042 ), #30808, .F. ) ;
#10814=AXIS2_PLACEMENT_3D ( 'NONE', #12850, #28239, #10676 ) ;
#10820=DIRECTION ( 'NONE',  ( 0.000000000000000000, 0.000000000000000000, 1.000000000000000000 ) ) ;
#10834=DIRECTION ( 'NONE',  ( -1.000000000000000000, 1.387778780781444413E-14, 0.000000000000000000 ) ) ;
#10837=EDGE_CURVE ( 'NONE', #27172, #974, #30297, .T. ) ;
#10845=ORIENTED_EDGE ( 'NONE', *, *, #10639, .T. ) ;
#10848=DIRECTION ( 'NONE',  ( 1.000000000000000000, -0.000000000000000000, 6.943123467126514267E-15 ) ) ;
#10861=VECTOR ( 'NONE', #28707, 1000.000000000000114 ) ;
#10875=CARTESIAN_POINT ( 'NONE',  ( 35.00000000000000000, 0.000000000000000000, -2.999999999999995559 ) ) ;
#10881=ORIENTED_EDGE ( 'NONE', *, *, #25250, .T. ) ;
#10886=DIRECTION ( 'NONE',  ( -1.211557572730276143E-16, -3.469446951953611428E-15, -1.000000000000000000 ) ) ;
#10908=EDGE_LOOP ( 'NONE', ( #10133, #5047, #20326, #17471 ) ) ;
#10909=AXIS2_PLACEMENT_3D ( 'NONE', #9977, #4796, #17657 ) ;
#10936=CIRCLE ( 'NONE', #12007, 7.981930256614262476 ) ;
#10947=DIRECTION ( 'NONE',  ( -0.000000000000000000, -1.000000000000000000, -0.000000000000000000 ) ) ;
#10989=EDGE_CURVE ( 'NONE', #24814, #17909, #23108, .T. ) ;
#11001=CARTESIAN_POINT ( 'NONE',  ( -12.44989959798873791, 6.043040383381309791E-17, -2.999999999999995559 ) ) ;
#11049=DIRECTION ( 'NONE',  ( -0.9993908270190956511, 0.03489949670250350189, -8.673617379884042375E-16 ) ) ;
#11076=ADVANCED_FACE ( 'NONE', ( #5513 ), #32209, .T. ) ;
#11118=DIRECTION ( 'NONE',  ( -0.000000000000000000, -1.000000000000000000, -0.000000000000000000 ) ) ;
#11165=EDGE_CURVE ( 'NONE', #14980, #26351, #11495, .T. ) ;
#11169=AXIS2_PLACEMENT_3D ( 'NONE', #939, #8602, #18640 ) ;
#11197=CARTESIAN_POINT ( 'NONE',  ( 34.48223484310472031, 0.5000000000000000000, -2.552009564962229859 ) ) ;
#11218=FACE_OUTER_BOUND ( 'NONE', #30989, .T. ) ;
#11236=DIRECTION ( 'NONE',  ( -3.028893931825485746E-17, -8.673617379884035472E-16, -1.000000000000000000 ) ) ;
#11253=AXIS2_PLACEMENT_3D ( 'NONE', #4834, #25560, #30777 ) ;
#11267=( NAMED_UNIT ( * ) SI_UNIT ( $, .STERADIAN. ) SOLID_ANGLE_UNIT ( ) );
#11291=DIRECTION ( 'NONE',  ( 0.000000000000000000, 1.000000000000000000, 0.000000000000000000 ) ) ;
#11293=VECTOR ( 'NONE', #33013, 1000.000000000000000 ) ;
#11302=CARTESIAN_POINT ( 'NONE',  ( -33.00121834596181714, -0.06979899340500209104, 3.000000000000004441 ) ) ;
#11307=AXIS2_PLACEMENT_3D ( 'NONE', #5225, #15576, #23282 ) ;
#11318=TOROIDAL_SURFACE ( 'NONE', #15591, 6.818740222761507042, 0.5000000000000000000 ) ;
#11325=EDGE_CURVE ( 'NONE', #17664, #30219, #4452, .T. ) ;
#11342=VECTOR ( 'NONE', #26224, 1000.000000000000227 ) ;
#11344=CARTESIAN_POINT ( 'NONE',  ( 12.44989959798868817, 0.4999999999999998890, 13.00000000000004441 ) ) ;
#11359=VECTOR ( 'NONE', #23348, 1000.000000000000114 ) ;
#11368=CARTESIAN_POINT ( 'NONE',  ( 34.55406472725060496, 0.5174497483512505713, -3.046515352619024508 ) ) ;
#11376=CIRCLE ( 'NONE', #184, 0.5000000000000004441 ) ;
#11390=AXIS2_PLACEMENT_3D ( 'NONE', #12166, #17673, #7321 ) ;
#11450=ORIENTED_EDGE ( 'NONE', *, *, #16499, .T. ) ;
#11453=PLANE ( 'NONE',  #15650 ) ;
#11459=FACE_OUTER_BOUND ( 'NONE', #22322, .T. ) ;
#11495=LINE ( 'NONE', #6646, #18858 ) ;
#11502=DIRECTION ( 'NONE',  ( -0.03488359650710489562, -0.9989355049964836475, 0.03018263660036206095 ) ) ;
#11538=LINE ( 'NONE', #6842, #17816 ) ;
#11554=CARTESIAN_POINT ( 'NONE',  ( -34.48223484310472031, 0.5000000000000000000, 2.552009564962237853 ) ) ;
#11580=DIRECTION ( 'NONE',  ( 0.9993908270190957621, 0.03489949670250105246, 3.467333458611667963E-15 ) ) ;
#11618=EDGE_CURVE ( 'NONE', #22141, #25215, #17807, .T. ) ;
#11620=CARTESIAN_POINT ( 'NONE',  ( 3.078042720788278785, 4.239848598108514111, -5.465019080499220472 ) ) ;
#11622=CARTESIAN_POINT ( 'NONE',  ( 0.000000000000000000, 20.00000000000000000, 0.000000000000000000 ) ) ;
#11632=EDGE_CURVE ( 'NONE', #29340, #8396, #15122, .T. ) ;
#11654=DIRECTION ( 'NONE',  ( 1.000000000000000000, 0.000000000000000000, 1.388624693425297016E-14 ) ) ;
#11688=DIRECTION ( 'NONE',  ( -0.1437473352845080599, 0.000000000000000000, 0.9896144216807893912 ) ) ;
#11692=VERTEX_POINT ( 'NONE', #19493 ) ;
#11693=CYLINDRICAL_SURFACE ( 'NONE', #22456, 0.5000000000000000000 ) ;
#11722=ADVANCED_FACE ( 'NONE', ( #6608 ), #18991, .F. ) ;
#11726=DIRECTION ( 'NONE',  ( 0.000000000000000000, -1.000000000000000000, 8.673617379884035472E-16 ) ) ;
#11778=CIRCLE ( 'NONE', #1101, 0.4999999999999997224 ) ;
#11817=DIRECTION ( 'NONE',  ( -0.000000000000000000, -1.000000000000000000, -0.000000000000000000 ) ) ;
#11850=EDGE_CURVE ( 'NONE', #8422, #29995, #24216, .T. ) ;
#11870=FACE_OUTER_BOUND ( 'NONE', #3305, .T. ) ;
#11881=AXIS2_PLACEMENT_3D ( 'NONE', #19848, #30057, #27686 ) ;
#11909=CARTESIAN_POINT ( 'NONE',  ( 0.000000000000000000, 37.67766952966368876, 0.000000000000000000 ) ) ;
#11969=CARTESIAN_POINT ( 'NONE',  ( -5.061877160328744907, 19.51744974835124324, -5.285536848417983435 ) ) ;
#11973=CARTESIAN_POINT ( 'NONE',  ( 5.240875073191910261, 0.000000000000000000, 3.405250132838362642 ) ) ;
#11976=EDGE_CURVE ( 'NONE', #3357, #30805, #3099, .T. ) ;
#11999=CARTESIAN_POINT ( 'NONE',  ( -3.936147556303791983, 18.00000000000000355, 4.854816414140053382 ) ) ;
#12007=AXIS2_PLACEMENT_3D ( 'NONE', #1057, #21939, #13899 ) ;
#12043=FACE_OUTER_BOUND ( 'NONE', #25123, .T. ) ;
#12044=ORIENTED_EDGE ( 'NONE', *, *, #28333, .T. ) ;
#12048=EDGE_CURVE ( 'NONE', #21127, #17768, #21138, .T. ) ;
#12067=DIRECTION ( 'NONE',  ( 0.005016709653754843068, -0.9993908270190956511, -0.03453704524619621158 ) ) ;
#12089=DIRECTION ( 'NONE',  ( -0.9896144216807905014, -0.000000000000000000, -0.1437473352845004826 ) ) ;
#12121=CARTESIAN_POINT ( 'NONE',  ( -5.561021557437524798, 7.493231324518994541, -2.854557343487579502 ) ) ;
#12125=VERTEX_POINT ( 'NONE', #31337 ) ;
#12127=CARTESIAN_POINT ( 'NONE',  ( -34.98193025661426248, 0.5174497483512505713, -2.482234843104711430 ) ) ;
#12147=ADVANCED_FACE ( 'NONE', ( #16770 ), #16417, .T. ) ;
#12150=PLANE ( 'NONE',  #16184 ) ;
#12166=CARTESIAN_POINT ( 'NONE',  ( -12.44989959798873791, 0.4999999999999998890, -12.99999999999999645 ) ) ;
#12211=CARTESIAN_POINT ( 'NONE',  ( -35.00000000000000000, 0.000000000000000000, 3.000000000000004441 ) ) ;
#12217=DIRECTION ( 'NONE',  ( 0.000000000000000000, 0.000000000000000000, -1.000000000000000000 ) ) ;
#12232=CARTESIAN_POINT ( 'NONE',  ( -35.00000000000000000, 0.000000000000000000, -2.999999999999995559 ) ) ;
#12251=EDGE_LOOP ( 'NONE', ( #5977, #8849, #15709, #4459 ) ) ;
#12258=ORIENTED_EDGE ( 'NONE', *, *, #9644, .F. ) ;
#12264=CIRCLE ( 'NONE', #16002, 0.4999999999999995559 ) ;
#12270=LINE ( 'NONE', #4606, #4348 ) ;
#12295=DIRECTION ( 'NONE',  ( -0.03488359650710490256, -0.9989355049964836475, 0.03018263660036206442 ) ) ;
#12324=FACE_OUTER_BOUND ( 'NONE', #32672, .T. ) ;
#12326=EDGE_CURVE ( 'NONE', #29752, #15174, #14894, .T. ) ;
#12343=DIRECTION ( 'NONE',  ( 0.000000000000000000, 0.000000000000000000, 1.000000000000000000 ) ) ;
#12349=DIRECTION ( 'NONE',  ( 6.938893903907228378E-15, 0.000000000000000000, -1.000000000000000000 ) ) ;
#12354=CARTESIAN_POINT ( 'NONE',  ( -3.526383166312414108, 10.27186380921760289, 5.187041768249671669 ) ) ;
#12356=VECTOR ( 'NONE', #15719, 1000.000000000000000 ) ;
#12359=AXIS2_PLACEMENT_3D ( 'NONE', #31897, #24196, #1320 ) ;
#12362=AXIS2_PLACEMENT_3D ( 'NONE', #28147, #10257, #31179 ) ;
#12399=VECTOR ( 'NONE', #32974, 1000.000000000000227 ) ;
#12405=CIRCLE ( 'NONE', #30038, 7.981930256614262476 ) ;
#12440=ADVANCED_FACE ( 'NONE', ( #18080 ), #10221, .T. ) ;
#12454=CARTESIAN_POINT ( 'NONE',  ( 0.000000000000000000, 0.5174497483512452423, 0.000000000000000000 ) ) ;
#12455=DIRECTION ( 'NONE',  ( 0.000000000000000000, 0.000000000000000000, -1.000000000000000000 ) ) ;
#12462=VECTOR ( 'NONE', #26567, 1000.000000000000114 ) ;
#12467=PRODUCT_DEFINITION_FORMATION_WITH_SPECIFIED_SOURCE ( 'ANY', '', #17492, .NOT_KNOWN. ) ;
#12471=EDGE_CURVE ( 'NONE', #27615, #4248, #15751, .T. ) ;
#12502=DESIGN_CONTEXT ( 'detailed design', #15441, 'design' ) ;
#12545=CARTESIAN_POINT ( 'NONE',  ( -34.31843563627105453, 19.51744974835125035, -2.301584610165037237 ) ) ;
#12577=CARTESIAN_POINT ( 'NONE',  ( 34.48223484310469900, 0.5000000000000000000, 2.482234843104950350 ) ) ;
#12578=DIRECTION ( 'NONE',  ( 1.000000000000000000, -0.000000000000000000, 8.654346879536960414E-15 ) ) ;
#12583=FACE_OUTER_BOUND ( 'NONE', #28561, .T. ) ;
#12617=EDGE_CURVE ( 'NONE', #29383, #27172, #27042, .T. ) ;
#12618=FACE_OUTER_BOUND ( 'NONE', #29677, .T. ) ;
#12620=EDGE_LOOP ( 'NONE', ( #8890, #5306, #28253, #27131, #4473 ) ) ;
#12627=CARTESIAN_POINT ( 'NONE',  ( 34.31843563627105453, 19.51744974835125035, -1.977928362984231025 ) ) ;
#12638=LINE ( 'NONE', #14806, #21930 ) ;
#12649=EDGE_CURVE ( 'NONE', #32461, #10785, #32791, .T. ) ;
#12705=DIRECTION ( 'NONE',  ( 0.000000000000000000, -1.000000000000000000, 0.000000000000000000 ) ) ;
#12724=DIRECTION ( 'NONE',  ( 0.03487826274237457863, -0.9987827659587182882, 0.03487826274237499496 ) ) ;
#12741=EDGE_CURVE ( 'NONE', #7166, #6030, #21039, .T. ) ;
#12768=ADVANCED_FACE ( 'NONE', ( #14817 ), #2479, .T. ) ;
#12793=CARTESIAN_POINT ( 'NONE',  ( -5.834205823644825095, 18.00000000000000355, -2.241549108841658366 ) ) ;
#12805=ORIENTED_EDGE ( 'NONE', *, *, #24551, .F. ) ;
#12814=EDGE_CURVE ( 'NONE', #29340, #22752, #19439, .T. ) ;
#12815=VERTEX_POINT ( 'NONE', #14668 ) ;
#12825=ORIENTED_EDGE ( 'NONE', *, *, #7758, .F. ) ;
#12848=VECTOR ( 'NONE', #30893, 1000.000000000000114 ) ;
#12850=CARTESIAN_POINT ( 'NONE',  ( 0.000000000000000000, 19.51744974835125035, 0.000000000000000000 ) ) ;
#12863=DIRECTION ( 'NONE',  ( 1.000000000000000000, 0.000000000000000000, 0.000000000000000000 ) ) ;
#12872=AXIS2_PLACEMENT_3D ( 'NONE', #22894, #25413, #2869 ) ;
#12899=VECTOR ( 'NONE', #4220, 1000.000000000000114 ) ;
#12919=ORIENTED_EDGE ( 'NONE', *, *, #7749, .T. ) ;
#12929=AXIS2_PLACEMENT_3D ( 'NONE', #30201, #14788, #20156 ) ;
#12936=VECTOR ( 'NONE', #15971, 1000.000000000000000 ) ;
#12951=CARTESIAN_POINT ( 'NONE',  ( -34.98223484310472031, 0.5000000000000000000, -2.482234843104711430 ) ) ;
#12958=AXIS2_PLACEMENT_3D ( 'NONE', #24068, #31950, #8529 ) ;
#12972=AXIS2_PLACEMENT_3D ( 'NONE', #30992, #18453, #7915 ) ;
#13009=AXIS2_PLACEMENT_3D ( 'NONE', #5466, #15658, #13142 ) ;
#13010=VERTEX_POINT ( 'NONE', #26368 ) ;
#13014=AXIS2_PLACEMENT_3D ( 'NONE', #10773, #3444, #5765 ) ;
#13055=DIRECTION ( 'NONE',  ( 1.000000000000000000, 0.000000000000000000, 0.000000000000000000 ) ) ;
#13080=CARTESIAN_POINT ( 'NONE',  ( 1.147424988311415595, 0.5000000000000000000, -7.899334717979326292 ) ) ;
#13083=AXIS2_PLACEMENT_3D ( 'NONE', #14352, #9685, #14710 ) ;
#13092=CARTESIAN_POINT ( 'NONE',  ( 34.50075980479081039, -0.03048549489923639208, -2.568038078148737302 ) ) ;
#13096=ORIENTED_EDGE ( 'NONE', *, *, #5441, .F. ) ;
#13141=DIRECTION ( 'NONE',  ( 0.1437473352844943209, -6.136584296267958883E-14, -0.9896144216807913896 ) ) ;
#13142=DIRECTION ( 'NONE',  ( 0.000000000000000000, 0.000000000000000000, -1.000000000000000000 ) ) ;
#13157=CARTESIAN_POINT ( 'NONE',  ( -12.44989959798873791, 0.000000000000000000, -12.99999999999999645 ) ) ;
#13181=ORIENTED_EDGE ( 'NONE', *, *, #29229, .F. ) ;
#13261=ORIENTED_EDGE ( 'NONE', *, *, #18046, .T. ) ;
#13274=CARTESIAN_POINT ( 'NONE',  ( 32.37020706055088937, 18.00000000000000355, 0.3702070605511125212 ) ) ;
#13287=DIRECTION ( 'NONE',  ( 0.7222222222222220989, 0.000000000000000000, -0.6916610887771519334 ) ) ;
#13310=ORIENTED_EDGE ( 'NONE', *, *, #26025, .F. ) ;
#13315=ORIENTED_EDGE ( 'NONE', *, *, #6890, .F. ) ;
#13381=CIRCLE ( 'NONE', #14985, 0.4999999999999996669 ) ;
#13382=DIRECTION ( 'NONE',  ( 0.9896144216807900573, -0.000000000000000000, 0.1437473352845036745 ) ) ;
#13420=ORIENTED_EDGE ( 'NONE', *, *, #7566, .F. ) ;
#13452=DIRECTION ( 'NONE',  ( 1.000000000000000000, -4.930380657631322689E-32, 8.654346879536960414E-15 ) ) ;
#13463=EDGE_CURVE ( 'NONE', #29021, #30219, #10936, .T. ) ;
#13475=CONICAL_SURFACE ( 'NONE', #7620, 8.000000000000000000, 0.03490658503988666728 ) ;
#13486=AXIS2_PLACEMENT_3D ( 'NONE', #12211, #4056, #14222 ) ;
#13495=CIRCLE ( 'NONE', #23646, 10.51776515689528502 ) ;
#13511=ORIENTED_EDGE ( 'NONE', *, *, #11632, .F. ) ;
#13521=CARTESIAN_POINT ( 'NONE',  ( 12.44989959798878232, 19.51744974835124680, 2.318435636271098943 ) ) ;
#13529=SHAPE_DEFINITION_REPRESENTATION ( #14545, #3460 ) ;
#13579=ADVANCED_FACE ( 'NONE', ( #27119 ), #3486, .T. ) ;
#13604=ORIENTED_EDGE ( 'NONE', *, *, #3841, .T. ) ;
#13608=ADVANCED_FACE ( 'NONE', ( #32339 ), #4572, .T. ) ;
#13619=CARTESIAN_POINT ( 'NONE',  ( -35.00000000000000000, -0.06979899340500209104, -1.001218345961804257 ) ) ;
#13623=LINE ( 'NONE', #19307, #21860 ) ;
#13636=FACE_OUTER_BOUND ( 'NONE', #24427, .T. ) ;
#13640=ORIENTED_EDGE ( 'NONE', *, *, #17437, .T. ) ;
#13656=CARTESIAN_POINT ( 'NONE',  ( -35.00000000000000000, 0.000000000000000000, -0.9987809114023521451 ) ) ;
#13684=ORIENTED_EDGE ( 'NONE', *, *, #21448, .F. ) ;
#13688=EDGE_CURVE ( 'NONE', #7632, #13010, #7746, .T. ) ;
#13704=CARTESIAN_POINT ( 'NONE',  ( -33.81874022276151948, 19.51744974835125035, -2.318435636271050537 ) ) ;
#13725=EDGE_LOOP ( 'NONE', ( #29305, #14348, #13310, #8210 ) ) ;
#13727=VERTEX_POINT ( 'NONE', #6847 ) ;
#13772=CARTESIAN_POINT ( 'NONE',  ( 0.000000000000000000, 0.000000000000000000, 0.000000000000000000 ) ) ;
#13773=CARTESIAN_POINT ( 'NONE',  ( 34.99999999999998579, 0.5174497483512504603, 2.981930256614502284 ) ) ;
#13774=CARTESIAN_POINT ( 'NONE',  ( -34.48223484310472742, 0.5000000000000000000, -2.482234843104710986 ) ) ;
#13783=LINE ( 'NONE', #9436, #19338 ) ;
#13839=ORIENTED_EDGE ( 'NONE', *, *, #28744, .T. ) ;
#13845=CIRCLE ( 'NONE', #14930, 0.4999999999999995559 ) ;
#13852=DIRECTION ( 'NONE',  ( 0.03488359650710505522, -0.9989355049964838695, -0.03018263660036221013 ) ) ;
#13882=ORIENTED_EDGE ( 'NONE', *, *, #23198, .T. ) ;
#13899=DIRECTION ( 'NONE',  ( 0.000000000000000000, 0.000000000000000000, 1.000000000000000000 ) ) ;
#13929=DIRECTION ( 'NONE',  ( 1.000000000000000000, -3.469446951953588156E-15, 1.053584095796274567E-14 ) ) ;
#13979=EDGE_CURVE ( 'NONE', #21819, #6075, #12638, .T. ) ;
#13992=VECTOR ( 'NONE', #7558, 1000.000000000000227 ) ;
#14001=AXIS2_PLACEMENT_3D ( 'NONE', #3534, #23893, #6183 ) ;
#14010=AXIS2_PLACEMENT_3D ( 'NONE', #23230, #5330, #8333 ) ;
#14012=EDGE_CURVE ( 'NONE', #8919, #29952, #32732, .T. ) ;
#14018=VECTOR ( 'NONE', #32616, 1000.000000000000000 ) ;
#14022=CARTESIAN_POINT ( 'NONE',  ( 5.561021557437512364, 7.493231324518997205, 2.854557343487603038 ) ) ;
#14039=AXIS2_PLACEMENT_3D ( 'NONE', #24975, #24637, #17114 ) ;
#14044=AXIS2_PLACEMENT_3D ( 'NONE', #2143, #17511, #14829 ) ;
#14046=AXIS2_PLACEMENT_3D ( 'NONE', #21549, #16349, #18539 ) ;
#14055=ORIENTED_EDGE ( 'NONE', *, *, #22335, .F. ) ;
#14062=EDGE_LOOP ( 'NONE', ( #8720, #19118, #29160, #27398 ) ) ;
#14070=ORIENTED_EDGE ( 'NONE', *, *, #6890, .T. ) ;
#14111=ORIENTED_EDGE ( 'NONE', *, *, #782, .F. ) ;
#14154=LINE ( 'NONE', #13656, #10771 ) ;
#14161=DIRECTION ( 'NONE',  ( 0.000000000000000000, -0.9993908270190956511, 0.03489949670250104552 ) ) ;
#14214=ORIENTED_EDGE ( 'NONE', *, *, #30405, .T. ) ;
#14219=EDGE_LOOP ( 'NONE', ( #26487, #30184, #914, #19213, #18911 ) ) ;
#14222=DIRECTION ( 'NONE',  ( -0.03489949670250104552, -0.9993908270190956511, 0.000000000000000000 ) ) ;
#14262=ADVANCED_FACE ( 'NONE', ( #2659 ), #8583, .T. ) ;
#14274=CYLINDRICAL_SURFACE ( 'NONE', #31067, 6.250000000000000000 ) ;
#14306=FACE_OUTER_BOUND ( 'NONE', #6285, .T. ) ;
#14308=DIRECTION ( 'NONE',  ( -8.649074885250573632E-15, 0.03489949670250105246, 0.9993908270190957621 ) ) ;
#14320=ORIENTED_EDGE ( 'NONE', *, *, #28987, .F. ) ;
#14327=ORIENTED_EDGE ( 'NONE', *, *, #24977, .F. ) ;
#14333=EDGE_LOOP ( 'NONE', ( #1953, #1468, #1400, #6600, #28563 ) ) ;
#14345=ORIENTED_EDGE ( 'NONE', *, *, #19783, .T. ) ;
#14348=ORIENTED_EDGE ( 'NONE', *, *, #24314, .F. ) ;
#14350=CARTESIAN_POINT ( 'NONE',  ( 5.521001242456709868, 0.4999999999999998890, 5.764947386686755770 ) ) ;
#14352=CARTESIAN_POINT ( 'NONE',  ( 12.44989959798868817, 20.00000000000000000, 13.00000000000004441 ) ) ;
#14361=ORIENTED_EDGE ( 'NONE', *, *, #27593, .T. ) ;
#14370=CARTESIAN_POINT ( 'NONE',  ( 1.149978682276028730, 0.000000000000000000, -7.916915373446320459 ) ) ;
#14374=CYLINDRICAL_SURFACE ( 'NONE', #28432, 6.250000000000000000 ) ;
#14378=ORIENTED_EDGE ( 'NONE', *, *, #25190, .T. ) ;
#14407=ORIENTED_EDGE ( 'NONE', *, *, #31622, .F. ) ;
#14435=AXIS2_PLACEMENT_3D ( 'NONE', #22776, #7546, #25601 ) ;
#14483=ADVANCED_FACE ( 'NONE', ( #18676 ), #5980, .F. ) ;
#14497=CIRCLE ( 'NONE', #31611, 0.5000000000000004441 ) ;
#14510=CARTESIAN_POINT ( 'NONE',  ( -34.99330891680700972, 0.1916075530515712055, -2.493613503297456901 ) ) ;
#14514=ORIENTED_EDGE ( 'NONE', *, *, #9626, .F. ) ;
#14545=PRODUCT_DEFINITION_SHAPE ( 'NONE', 'NONE',  #23132 ) ;
#14546=CONICAL_SURFACE ( 'NONE', #31147, 10.00000000000000178, 0.03490658503988666728 ) ;
#14591=PLANE ( 'NONE',  #20390 ) ;
#14645=ORIENTED_EDGE ( 'NONE', *, *, #18703, .T. ) ;
#14649=EDGE_CURVE ( 'NONE', #17768, #29452, #16067, .T. ) ;
#14656=ORIENTED_EDGE ( 'NONE', *, *, #18117, .T. ) ;
#14668=CARTESIAN_POINT ( 'NONE',  ( -34.98223484310472031, 0.5000000000000000000, 2.552009564962238297 ) ) ;
#14697=EDGE_CURVE ( 'NONE', #24965, #29752, #29721, .T. ) ;
#14700=ORIENTED_EDGE ( 'NONE', *, *, #23360, .T. ) ;
#14710=DIRECTION ( 'NONE',  ( 1.706601815529740836E-15, 0.000000000000000000, 1.000000000000000000 ) ) ;
#14732=FACE_OUTER_BOUND ( 'NONE', #28691, .T. ) ;
#14749=CARTESIAN_POINT ( 'NONE',  ( 12.44989959798879831, -0.06979899340500890503, 1.001218345961853107 ) ) ;
#14753=CARTESIAN_POINT ( 'NONE',  ( -12.44989959798873791, 0.5174497483512504603, -2.981930256614258923 ) ) ;
#14774=CARTESIAN_POINT ( 'NONE',  ( 5.834205823644816213, 18.00000000000000355, 2.241549108841682791 ) ) ;
#14778=CARTESIAN_POINT ( 'NONE',  ( -34.48223484310472742, 0.5000000000000000000, -2.982234843104710986 ) ) ;
#14785=CARTESIAN_POINT ( 'NONE',  ( -5.323856294847543857, 1.496472198897157213, -3.277537277937041527 ) ) ;
#14788=DIRECTION ( 'NONE',  ( -3.469446951953478110E-15, 0.000000000000000000, 1.000000000000000000 ) ) ;
#14796=CARTESIAN_POINT ( 'NONE',  ( 0.000000000000000000, 0.000000000000000000, 0.000000000000000000 ) ) ;
#14806=CARTESIAN_POINT ( 'NONE',  ( -34.99744630603539974, 0.5000000000000000000, 2.982419344533008498 ) ) ;
#14817=FACE_OUTER_BOUND ( 'NONE', #5990, .T. ) ;
#14829=DIRECTION ( 'NONE',  ( 0.000000000000000000, 0.000000000000000000, 1.000000000000000000 ) ) ;
#14848=CYLINDRICAL_SURFACE ( 'NONE', #22448, 0.5000000000000000000 ) ;
#14868=DIRECTION ( 'NONE',  ( 0.9896144216807900573, 0.000000000000000000, 0.1437473352845035912 ) ) ;
#14875=ORIENTED_EDGE ( 'NONE', *, *, #31420, .T. ) ;
#14892=ORIENTED_EDGE ( 'NONE', *, *, #33071, .T. ) ;
#14894=LINE ( 'NONE', #4724, #759 ) ;
#14902=FACE_OUTER_BOUND ( 'NONE', #3414, .T. ) ;
#14910=EDGE_LOOP ( 'NONE', ( #23091, #24422, #1924, #12825 ) ) ;
#14914=ORIENTED_EDGE ( 'NONE', *, *, #20004, .T. ) ;
#14919=CARTESIAN_POINT ( 'NONE',  ( 34.48223484310469900, 0.5000000000000000000, 2.482234843104950350 ) ) ;
#14930=AXIS2_PLACEMENT_3D ( 'NONE', #30701, #2086, #30010 ) ;
#14946=CARTESIAN_POINT ( 'NONE',  ( 3.936147556303794648, 18.00000000000000355, -4.854816414140051606 ) ) ;
#14956=VERTEX_POINT ( 'NONE', #1230 ) ;
#14980=VERTEX_POINT ( 'NONE', #26479 ) ;
#14985=AXIS2_PLACEMENT_3D ( 'NONE', #9434, #29846, #32527 ) ;
#15006=ORIENTED_EDGE ( 'NONE', *, *, #24264, .T. ) ;
#15012=ORIENTED_EDGE ( 'NONE', *, *, #7124, .F. ) ;
#15073=VECTOR ( 'NONE', #31155, 1000.000000000000000 ) ;
#15083=DIRECTION ( 'NONE',  ( 1.040834085586084257E-14, 0.000000000000000000, -1.000000000000000000 ) ) ;
#15111=VERTEX_POINT ( 'NONE', #24938 ) ;
#15122=CIRCLE ( 'NONE', #9246, 0.4999999999999997224 ) ;
#15174=VERTEX_POINT ( 'NONE', #13704 ) ;
#15175=EDGE_CURVE ( 'NONE', #8736, #21127, #14497, .T. ) ;
#15184=DIRECTION ( 'NONE',  ( -1.000000000000000000, 4.930380657631322689E-32, -8.654346879536960414E-15 ) ) ;
#15201=ORIENTED_EDGE ( 'NONE', *, *, #19764, .T. ) ;
#15202=AXIS2_PLACEMENT_3D ( 'NONE', #12577, #27470, #17274 ) ;
#15212=EDGE_CURVE ( 'NONE', #30805, #26351, #18786, .T. ) ;
#15221=PLANE ( 'NONE',  #5494 ) ;
#15236=VERTEX_POINT ( 'NONE', #21583 ) ;
#15241=CARTESIAN_POINT ( 'NONE',  ( -34.48223484310472031, 0.000000000000000000, 13.00000000000004441 ) ) ;
#15262=ORIENTED_EDGE ( 'NONE', *, *, #20033, .T. ) ;
#15295=ORIENTED_EDGE ( 'NONE', *, *, #22819, .T. ) ;
#15297=DIRECTION ( 'NONE',  ( 0.000000000000000000, 0.000000000000000000, 1.000000000000000000 ) ) ;
#15304=EDGE_LOOP ( 'NONE', ( #29611, #5671, #18214, #17548 ) ) ;
#15361=DIRECTION ( 'NONE',  ( 0.000000000000000000, 0.000000000000000000, -1.000000000000000000 ) ) ;
#15374=FACE_OUTER_BOUND ( 'NONE', #21779, .T. ) ;
#15392=DIRECTION ( 'NONE',  ( 0.000000000000000000, 0.000000000000000000, 1.000000000000000000 ) ) ;
#15431=DIRECTION ( 'NONE',  ( 0.9896144216807899463, -0.000000000000000000, 0.1437473352845035635 ) ) ;
#15441=APPLICATION_CONTEXT ( 'configuration controlled 3d designs of mechanical parts and assemblies' ) ;
#15464=DIRECTION ( 'NONE',  ( 0.000000000000000000, 0.9993908270190956511, 0.03489949670250104552 ) ) ;
#15519=CARTESIAN_POINT ( 'NONE',  ( 12.44989959798868817, 0.000000000000000000, 13.00000000000004441 ) ) ;
#15528=AXIS2_PLACEMENT_3D ( 'NONE', #13619, #23823, #15464 ) ;
#15531=VECTOR ( 'NONE', #18155, 1000.000000000000227 ) ;
#15541=EDGE_CURVE ( 'NONE', #13010, #9377, #28927, .T. ) ;
#15568=DIRECTION ( 'NONE',  ( -1.000000000000000000, 0.000000000000000000, -0.000000000000000000 ) ) ;
#15570=EDGE_CURVE ( 'NONE', #8422, #9245, #15998, .T. ) ;
#15576=DIRECTION ( 'NONE',  ( 0.000000000000000000, 0.000000000000000000, -1.000000000000000000 ) ) ;
#15591=AXIS2_PLACEMENT_3D ( 'NONE', #3877, #29623, #21749 ) ;
#15614=DIRECTION ( 'NONE',  ( 0.03488359650710500665, -0.9989355049964836475, -0.03018263660036204013 ) ) ;
#15618=CIRCLE ( 'NONE', #144, 0.5000000000000004441 ) ;
#15624=DIRECTION ( 'NONE',  ( 0.000000000000000000, -1.000000000000000000, 0.000000000000000000 ) ) ;
#15628=EDGE_CURVE ( 'NONE', #974, #20282, #26289, .T. ) ;
#15637=AXIS2_PLACEMENT_3D ( 'NONE', #20981, #10947, #20809 ) ;
#15650=AXIS2_PLACEMENT_3D ( 'NONE', #29321, #21649, #9078 ) ;
#15658=DIRECTION ( 'NONE',  ( -0.000000000000000000, -1.000000000000000000, -0.000000000000000000 ) ) ;
#15667=TOROIDAL_SURFACE ( 'NONE', #14044, 10.51776515689528502, 0.5000000000000000000 ) ;
#15678=EDGE_LOOP ( 'NONE', ( #29228, #12258, #9641, #32229 ) ) ;
#15687=ORIENTED_EDGE ( 'NONE', *, *, #7313, .T. ) ;
#15709=ORIENTED_EDGE ( 'NONE', *, *, #30660, .F. ) ;
#15719=DIRECTION ( 'NONE',  ( -1.000000000000000000, 0.000000000000000000, -0.000000000000000000 ) ) ;
#15751=LINE ( 'NONE', #28121, #1306 ) ;
#15771=CARTESIAN_POINT ( 'NONE',  ( -34.30400690026458221, 19.51744974835125035, 2.412380016372531522 ) ) ;
#15779=PLANE ( 'NONE',  #12362 ) ;
#15782=ORIENTED_EDGE ( 'NONE', *, *, #12617, .F. ) ;
#15817=CARTESIAN_POINT ( 'NONE',  ( -12.44989959798873791, 0.5174497483512729978, -12.99999999999999645 ) ) ;
#15837=DIRECTION ( 'NONE',  ( 0.000000000000000000, 0.000000000000000000, 1.000000000000000000 ) ) ;
#15886=EDGE_LOOP ( 'NONE', ( #13261, #25465, #20284, #11450 ) ) ;
#15916=VERTEX_POINT ( 'NONE', #12793 ) ;
#15929=CARTESIAN_POINT ( 'NONE',  ( 34.57258968893669504, -0.01303574654798587279, -3.062543865805531951 ) ) ;
#15971=DIRECTION ( 'NONE',  ( 3.469446951953478110E-15, -0.000000000000000000, -1.000000000000000000 ) ) ;
#15976=CIRCLE ( 'NONE', #4776, 10.01776515689528502 ) ;
#15983=CIRCLE ( 'NONE', #5846, 0.5000000000000000000 ) ;
#15986=EDGE_CURVE ( 'NONE', #8919, #27372, #27269, .T. ) ;
#15998=LINE ( 'NONE', #21061, #11342 ) ;
#16002=AXIS2_PLACEMENT_3D ( 'NONE', #8604, #3467, #23670 ) ;
#16021=CIRCLE ( 'NONE', #3759, 10.51776515689528502 ) ;
#16029=CARTESIAN_POINT ( 'NONE',  ( 0.000000000000000000, 19.51744974835125035, 0.000000000000000000 ) ) ;
#16067=CIRCLE ( 'NONE', #12359, 6.818740222761507042 ) ;
#16076=CIRCLE ( 'NONE', #1688, 0.5000000000000004441 ) ;
#16127=FACE_OUTER_BOUND ( 'NONE', #15678, .T. ) ;
#16129=ORIENTED_EDGE ( 'NONE', *, *, #3302, .T. ) ;
#16130=AXIS2_PLACEMENT_3D ( 'NONE', #3166, #8654, #29219 ) ;
#16155=CIRCLE ( 'NONE', #1758, 0.5000000000000000000 ) ;
#16158=DIRECTION ( 'NONE',  ( 0.000000000000000000, 1.000000000000000000, 0.000000000000000000 ) ) ;
#16184=AXIS2_PLACEMENT_3D ( 'NONE', #32407, #14308, #14161 ) ;
#16192=FACE_OUTER_BOUND ( 'NONE', #32138, .T. ) ;
#16203=CARTESIAN_POINT ( 'NONE',  ( 0.9801757370192288876, 20.00000000000000000, -6.747923662139670320 ) ) ;
#16206=DIRECTION ( 'NONE',  ( 0.000000000000000000, 6.938893903907228378E-15, 1.000000000000000000 ) ) ;
#16210=VERTEX_POINT ( 'NONE', #14778 ) ;
#16229=DIRECTION ( 'NONE',  ( 0.000000000000000000, 0.000000000000000000, 1.000000000000000000 ) ) ;
#16242=DIRECTION ( 'NONE',  ( 0.000000000000000000, 0.000000000000000000, 1.000000000000000000 ) ) ;
#16265=CARTESIAN_POINT ( 'NONE',  ( 34.31843563627104743, 19.51744974835125035, 1.818740222761737302 ) ) ;
#16272=DIRECTION ( 'NONE',  ( 0.000000000000000000, 1.000000000000000000, 0.000000000000000000 ) ) ;
#16282=APPLICATION_CONTEXT ( 'configuration controlled 3d designs of mechanical parts and assemblies' ) ;
#16306=CARTESIAN_POINT ( 'NONE',  ( 12.44989959798868817, 18.00000000000000355, 13.00000000000004441 ) ) ;
#16349=DIRECTION ( 'NONE',  ( -3.028893931825485746E-17, -8.673617379884035472E-16, -1.000000000000000000 ) ) ;
#16382=ORIENTED_EDGE ( 'NONE', *, *, #16546, .T. ) ;
#16417=PLANE ( 'NONE',  #31712 ) ;
#16434=ORIENTED_EDGE ( 'NONE', *, *, #21763, .F. ) ;
#16462=VERTEX_POINT ( 'NONE', #14350 ) ;
#16492=LINE ( 'NONE', #19181, #84 ) ;
#16499=EDGE_CURVE ( 'NONE', #9377, #18687, #32110, .T. ) ;
#16500=CARTESIAN_POINT ( 'NONE',  ( -34.98193025661426248, 0.5174497483512504603, 3.000000000000004441 ) ) ;
#16503=CONICAL_SURFACE ( 'NONE', #11169, 11.99878165403819352, 0.03490658503988666728 ) ;
#16514=ADVANCED_FACE ( 'NONE', ( #17894 ), #30427, .T. ) ;
#16519=CARTESIAN_POINT ( 'NONE',  ( 5.699736881468946414, 11.99440202994180993, 2.572806452144735356 ) ) ;
#16539=EDGE_CURVE ( 'NONE', #11692, #10028, #606, .T. ) ;
#16544=DIRECTION ( 'NONE',  ( 1.387778780781445676E-14, 0.000000000000000000, 1.000000000000000000 ) ) ;
#16546=EDGE_CURVE ( 'NONE', #5629, #22098, #185, .T. ) ;
#16556=ORIENTED_EDGE ( 'NONE', *, *, #24471, .F. ) ;
#16572=AXIS2_PLACEMENT_3D ( 'NONE', #25943, #10886, #515 ) ;
#16606=ORIENTED_EDGE ( 'NONE', *, *, #2626, .F. ) ;
#16616=VECTOR ( 'NONE', #21940, 1000.000000000000114 ) ;
#16634=DIRECTION ( 'NONE',  ( -0.03489949670250104552, -0.9993908270190956511, 0.000000000000000000 ) ) ;
#16645=CIRCLE ( 'NONE', #27350, 0.4999999999999997780 ) ;
#16702=CIRCLE ( 'NONE', #24724, 7.482234843104714983 ) ;
#16717=CARTESIAN_POINT ( 'NONE',  ( -33.81874022276151237, 19.50000000000000000, 1.977928362984239019 ) ) ;
#16723=ADVANCED_FACE ( 'NONE', ( #16192 ), #3825, .T. ) ;
#16755=CIRCLE ( 'NONE', #26900, 0.5000000000000000000 ) ;
#16770=FACE_OUTER_BOUND ( 'NONE', #12251, .T. ) ;
#16797=EDGE_LOOP ( 'NONE', ( #6389, #13420, #14070, #20140 ) ) ;
#16807=FACE_OUTER_BOUND ( 'NONE', #10908, .T. ) ;
#16857=LINE ( 'NONE', #24374, #7644 ) ;
#16894=CYLINDRICAL_SURFACE ( 'NONE', #17187, 0.5000000000000004441 ) ;
#16903=ORIENTED_EDGE ( 'NONE', *, *, #5481, .T. ) ;
#16928=ORIENTED_EDGE ( 'NONE', *, *, #2900, .F. ) ;
#16995=CARTESIAN_POINT ( 'NONE',  ( -33.00303921916323446, -0.1219419795969449855, 1.272152312594969414 ) ) ;
#17011=ORIENTED_EDGE ( 'NONE', *, *, #28175, .T. ) ;
#17025=CARTESIAN_POINT ( 'NONE',  ( -34.92557263839314885, 0.5000000000000000000, 2.487612133692613359 ) ) ;
#17045=VECTOR ( 'NONE', #25628, 1000.000000000000000 ) ;
#17114=DIRECTION ( 'NONE',  ( -1.000000000000000000, 0.000000000000000000, -3.469446951953611033E-15 ) ) ;
#17137=CARTESIAN_POINT ( 'NONE',  ( -12.44989959798873791, 0.000000000000000000, -0.9987809114023521451 ) ) ;
#17170=ADVANCED_FACE ( 'NONE', ( #949 ), #21026, .T. ) ;
#17176=CIRCLE ( 'NONE', #7559, 0.4999999999999995559 ) ;
#17183=AXIS2_PLACEMENT_3D ( 'NONE', #11197, #13852, #31300 ) ;
#17187=AXIS2_PLACEMENT_3D ( 'NONE', #4045, #26759, #32124 ) ;
#17217=CIRCLE ( 'NONE', #27356, 0.5000000000000000000 ) ;
#17231=AXIS2_PLACEMENT_3D ( 'NONE', #3947, #29174, #29511 ) ;
#17234=CIRCLE ( 'NONE', #9195, 0.5000000000000000000 ) ;
#17244=AXIS2_PLACEMENT_3D ( 'NONE', #17555, #12863, #10197 ) ;
#17253=ORIENTED_EDGE ( 'NONE', *, *, #3841, .F. ) ;
#17274=DIRECTION ( 'NONE',  ( 0.000000000000000000, 0.000000000000000000, -1.000000000000000000 ) ) ;
#17292=ORIENTED_EDGE ( 'NONE', *, *, #7361, .T. ) ;
#17300=LINE ( 'NONE', #27495, #19934 ) ;
#17311=CARTESIAN_POINT ( 'NONE',  ( 33.81874022276149816, 20.00000000000000000, 1.818740222761736414 ) ) ;
#17328=ORIENTED_EDGE ( 'NONE', *, *, #22164, .T. ) ;
#17332=ORIENTED_EDGE ( 'NONE', *, *, #21355, .F. ) ;
#17343=EDGE_CURVE ( 'NONE', #15916, #20282, #24085, .T. ) ;
#17371=EDGE_CURVE ( 'NONE', #22830, #28234, #24523, .T. ) ;
#17437=EDGE_CURVE ( 'NONE', #30219, #22141, #12405, .T. ) ;
#17445=CARTESIAN_POINT ( 'NONE',  ( -5.240875073191923583, 0.000000000000000000, -3.405250132838343102 ) ) ;
#17461=DIRECTION ( 'NONE',  ( 0.000000000000000000, 0.000000000000000000, -1.000000000000000000 ) ) ;
#17464=EDGE_CURVE ( 'NONE', #22830, #8298, #30574, .T. ) ;
#17469=CYLINDRICAL_SURFACE ( 'NONE', #1255, 0.5000000000000004441 ) ;
#17471=ORIENTED_EDGE ( 'NONE', *, *, #17371, .T. ) ;
#17492=PRODUCT ( 'Part6_handleknob', 'Part6_handleknob', '', ( #3038 ) ) ;
#17511=DIRECTION ( 'NONE',  ( 0.000000000000000000, 1.000000000000000000, 0.000000000000000000 ) ) ;
#17515=CARTESIAN_POINT ( 'NONE',  ( -34.48223484310472742, 0.5174497483512505713, -2.981930256614258923 ) ) ;
#17525=ADVANCED_FACE ( 'NONE', ( #25086 ), #14374, .T. ) ;
#17540=ADVANCED_FACE ( 'NONE', ( #14732 ), #22606, .T. ) ;
#17548=ORIENTED_EDGE ( 'NONE', *, *, #8146, .F. ) ;
#17555=CARTESIAN_POINT ( 'NONE',  ( 33.81874022276149816, 19.50000000000000000, 1.818740222761735970 ) ) ;
#17619=DIRECTION ( 'NONE',  ( 0.000000000000000000, 1.000000000000000000, 0.000000000000000000 ) ) ;
#17622=DIRECTION ( 'NONE',  ( 1.000000000000000000, -0.000000000000000000, 8.654346879536960414E-15 ) ) ;
#17646=AXIS2_PLACEMENT_3D ( 'NONE', #24737, #19903, #9505 ) ;
#17657=DIRECTION ( 'NONE',  ( 1.776356839400250465E-15, 0.000000000000000000, 1.000000000000000000 ) ) ;
#17664=VERTEX_POINT ( 'NONE', #23800 ) ;
#17669=VECTOR ( 'NONE', #15624, 1000.000000000000000 ) ;
#17673=DIRECTION ( 'NONE',  ( 0.000000000000000000, 1.000000000000000000, 0.000000000000000000 ) ) ;
#17676=AXIS2_PLACEMENT_3D ( 'NONE', #21548, #29223, #23542 ) ;
#17684=AXIS2_PLACEMENT_3D ( 'NONE', #20823, #110, #10299 ) ;
#17705=CIRCLE ( 'NONE', #27848, 10.68156436372894724 ) ;
#17753=AXIS2_PLACEMENT_3D ( 'NONE', #5056, #5368, #5207 ) ;
#17768=VERTEX_POINT ( 'NONE', #4221 ) ;
#17804=CARTESIAN_POINT ( 'NONE',  ( 4.592425496802574958E-16, 37.67766952966368876, 3.750000000000000444 ) ) ;
#17807=CIRCLE ( 'NONE', #13009, 10.01806974338573752 ) ;
#17816=VECTOR ( 'NONE', #24902, 1000.000000000000114 ) ;
#17890=PLANE ( 'NONE',  #3289 ) ;
#17894=FACE_OUTER_BOUND ( 'NONE', #7886, .T. ) ;
#17909=VERTEX_POINT ( 'NONE', #17936 ) ;
#17927=CARTESIAN_POINT ( 'NONE',  ( 12.44989959798868817, 0.000000000000000000, 13.00000000000004441 ) ) ;
#17934=DIRECTION ( 'NONE',  ( 0.9993908270190957621, -0.03489949670250105940, 0.000000000000000000 ) ) ;
#17936=CARTESIAN_POINT ( 'NONE',  ( -1.052005621165114313, 19.51744974835124680, 7.242429449796464525 ) ) ;
#17947=ADVANCED_FACE ( 'NONE', ( #27970 ), #26319, .F. ) ;
#17999=DIRECTION ( 'NONE',  ( 3.469446951953478110E-15, 0.000000000000000000, -1.000000000000000000 ) ) ;
#18013=DIRECTION ( 'NONE',  ( -0.03487826274237457169, 0.9987827659587181772, -0.03487826274237498803 ) ) ;
#18030=CARTESIAN_POINT ( 'NONE',  ( -2.598264985223428969, 0.000000000000000000, 5.684322216989629695 ) ) ;
#18046=EDGE_CURVE ( 'NONE', #18687, #22141, #23283, .T. ) ;
#18049=ADVANCED_FACE ( 'NONE', ( #28277 ), #13475, .T. ) ;
#18080=FACE_OUTER_BOUND ( 'NONE', #3128, .T. ) ;
#18108=CARTESIAN_POINT ( 'NONE',  ( -34.48223484310472031, 0.000000000000000000, 2.552009564962238741 ) ) ;
#18114=CARTESIAN_POINT ( 'NONE',  ( -1.075551320669168254, 0.4999999999999998890, 7.404527507138928932 ) ) ;
#18117=EDGE_CURVE ( 'NONE', #22098, #21127, #2921, .T. ) ;
#18146=ORIENTED_EDGE ( 'NONE', *, *, #18882, .F. ) ;
#18155=DIRECTION ( 'NONE',  ( 0.9896144216807899463, -0.000000000000000000, 0.1437473352845035635 ) ) ;
#18214=ORIENTED_EDGE ( 'NONE', *, *, #19764, .F. ) ;
#18218=CARTESIAN_POINT ( 'NONE',  ( 34.99330891680699551, 0.1916075530515802261, 2.493613503297696266 ) ) ;
#18244=ORIENTED_EDGE ( 'NONE', *, *, #24917, .T. ) ;
#18250=CARTESIAN_POINT ( 'NONE',  ( -34.50075980479081039, -0.03048549489923630187, 2.568038078148746184 ) ) ;
#18256=DIRECTION ( 'NONE',  ( 1.000000000000000000, -3.469446951953588156E-15, 1.053584095796274567E-14 ) ) ;
#18259=AXIS2_PLACEMENT_3D ( 'NONE', #31056, #805, #3141 ) ;
#18265=FACE_OUTER_BOUND ( 'NONE', #18375, .T. ) ;
#18274=EDGE_CURVE ( 'NONE', #18687, #24814, #22594, .T. ) ;
#18305=FACE_OUTER_BOUND ( 'NONE', #5735, .T. ) ;
#18326=ORIENTED_EDGE ( 'NONE', *, *, #18882, .T. ) ;
#18351=CARTESIAN_POINT ( 'NONE',  ( 34.71233008869360503, 0.000000000000000000, -1.019564728980880908 ) ) ;
#18363=DIRECTION ( 'NONE',  ( 0.000000000000000000, 1.000000000000000000, 0.000000000000000000 ) ) ;
#18371=DIRECTION ( 'NONE',  ( -0.6916610887771532656, 0.000000000000000000, -0.7222222222222208776 ) ) ;
#18374=AXIS2_PLACEMENT_3D ( 'NONE', #10875, #8022, #8508 ) ;
#18375=EDGE_LOOP ( 'NONE', ( #6756, #5402, #9422, #8903 ) ) ;
#18453=DIRECTION ( 'NONE',  ( 0.9896144216807901683, -0.000000000000000000, 0.1437473352845036190 ) ) ;
#18473=CARTESIAN_POINT ( 'NONE',  ( 32.37020706055089647, 18.00000000000000355, -0.7246014581832489476 ) ) ;
#18534=DIRECTION ( 'NONE',  ( 0.000000000000000000, -1.000000000000000000, 0.000000000000000000 ) ) ;
#18539=DIRECTION ( 'NONE',  ( -1.387778780781445676E-14, -1.000000000000000000, 8.673617379884035472E-16 ) ) ;
#18555=ORIENTED_EDGE ( 'NONE', *, *, #10499, .F. ) ;
#18605=CARTESIAN_POINT ( 'NONE',  ( -32.99635089100451069, 0.06958667959533217096, -0.9963508910045062450 ) ) ;
#18608=CARTESIAN_POINT ( 'NONE',  ( -33.81874022276151237, 20.00000000000000000, -1.818740222761504599 ) ) ;
#18640=DIRECTION ( 'NONE',  ( 0.000000000000000000, 0.000000000000000000, 1.000000000000000000 ) ) ;
#18652=LINE ( 'NONE', #18351, #25201 ) ;
#18676=FACE_OUTER_BOUND ( 'NONE', #6107, .T. ) ;
#18682=AXIS2_PLACEMENT_3D ( 'NONE', #25673, #17999, #22841 ) ;
#18687=VERTEX_POINT ( 'NONE', #30937 ) ;
#18703=EDGE_CURVE ( 'NONE', #15236, #27172, #3356, .T. ) ;
#18712=CARTESIAN_POINT ( 'NONE',  ( 5.834205823644816213, 18.00000000000000355, 2.241549108841682791 ) ) ;
#18738=CARTESIAN_POINT ( 'NONE',  ( 0.000000000000000000, 0.000000000000000000, 0.000000000000000000 ) ) ;
#18744=EDGE_LOOP ( 'NONE', ( #3282, #22919, #9865, #13839 ) ) ;
#18786=CIRCLE ( 'NONE', #17183, 0.4999999999999995559 ) ;
#18794=DIRECTION ( 'NONE',  ( 0.000000000000000000, 0.000000000000000000, 1.000000000000000000 ) ) ;
#18821=CARTESIAN_POINT ( 'NONE',  ( 12.44989959798878232, 0.4999999999999998890, 2.482234843104758060 ) ) ;
#18831=DIRECTION ( 'NONE',  ( 0.000000000000000000, 1.000000000000000000, 0.000000000000000000 ) ) ;
#18842=EDGE_CURVE ( 'NONE', #30055, #8068, #8674, .T. ) ;
#18848=LINE ( 'NONE', #31389, #10861 ) ;
#18858=VECTOR ( 'NONE', #1814, 1000.000000000000000 ) ;
#18870=DIRECTION ( 'NONE',  ( 0.000000000000000000, -1.000000000000000000, 0.000000000000000000 ) ) ;
#18882=EDGE_CURVE ( 'NONE', #24347, #8396, #20480, .T. ) ;
#18884=ORIENTED_EDGE ( 'NONE', *, *, #15175, .T. ) ;
#18885=ADVANCED_FACE ( 'NONE', ( #12324 ), #15667, .T. ) ;
#18905=ORIENTED_EDGE ( 'NONE', *, *, #25914, .F. ) ;
#18911=ORIENTED_EDGE ( 'NONE', *, *, #2603, .F. ) ;
#18919=ORIENTED_EDGE ( 'NONE', *, *, #7544, .F. ) ;
#18991=PLANE ( 'NONE',  #2334 ) ;
#18994=DIRECTION ( 'NONE',  ( -1.000000000000000000, 0.000000000000000000, -8.673617379884027583E-16 ) ) ;
#19039=ORIENTED_EDGE ( 'NONE', *, *, #25482, .F. ) ;
#19056=EDGE_LOOP ( 'NONE', ( #2078, #22803, #14327, #32605 ) ) ;
#19082=ORIENTED_EDGE ( 'NONE', *, *, #4266, .F. ) ;
#19118=ORIENTED_EDGE ( 'NONE', *, *, #12326, .F. ) ;
#19138=CARTESIAN_POINT ( 'NONE',  ( 34.99999999999999289, -0.06979899340500209104, 1.001218345962048062 ) ) ;
#19157=VERTEX_POINT ( 'NONE', #25850 ) ;
#19174=CARTESIAN_POINT ( 'NONE',  ( -35.00000000000000000, 0.5174497483512504603, -2.981930256614258923 ) ) ;
#19176=CARTESIAN_POINT ( 'NONE',  ( 34.48223484310469900, 0.5000000000000001110, 2.482234843104949462 ) ) ;
#19181=CARTESIAN_POINT ( 'NONE',  ( 12.44989959798877699, 0.000000000000000000, 3.000000000000044409 ) ) ;
#19207=DIRECTION ( 'NONE',  ( 1.000000000000000000, 0.000000000000000000, 1.388624693425297016E-14 ) ) ;
#19213=ORIENTED_EDGE ( 'NONE', *, *, #7278, .F. ) ;
#19232=CIRCLE ( 'NONE', #29392, 0.5000000000000000000 ) ;
#19266=ORIENTED_EDGE ( 'NONE', *, *, #24186, .F. ) ;
#19294=CIRCLE ( 'NONE', #17684, 12.62979293944910353 ) ;
#19297=DIRECTION ( 'NONE',  ( 0.1437473352845037022, 0.000000000000000000, -0.9896144216807900573 ) ) ;
#19307=CARTESIAN_POINT ( 'NONE',  ( 34.62197427260419147, 18.00000000000000355, -0.3975189810868455798 ) ) ;
#19312=AXIS2_PLACEMENT_3D ( 'NONE', #10272, #10595, #20799 ) ;
#19323=CARTESIAN_POINT ( 'NONE',  ( 3.936147556303794648, 18.00000000000000355, -4.854816414140051606 ) ) ;
#19338=VECTOR ( 'NONE', #21816, 1000.000000000000000 ) ;
#19348=CARTESIAN_POINT ( 'NONE',  ( 0.000000000000000000, 18.00000000000000355, 0.000000000000000000 ) ) ;
#19365=DIRECTION ( 'NONE',  ( -3.020323503847002675E-16, -0.9993908270190956511, 0.03489949670250104552 ) ) ;
#19415=AXIS2_PLACEMENT_3D ( 'NONE', #11554, #21598, #21421 ) ;
#19425=DIRECTION ( 'NONE',  ( -1.000000000000000000, 0.000000000000000000, -8.673617379884027583E-16 ) ) ;
#19433=FACE_OUTER_BOUND ( 'NONE', #9571, .T. ) ;
#19439=CIRCLE ( 'NONE', #10909, 7.482234843104714983 ) ;
#19442=FACE_OUTER_BOUND ( 'NONE', #5282, .T. ) ;
#19448=CARTESIAN_POINT ( 'NONE',  ( -12.44989959798873791, 0.5000000000000000000, -2.482234843104710986 ) ) ;
#19462=CARTESIAN_POINT ( 'NONE',  ( 4.716257286563768858, 20.00000000000000000, 4.924645716438879717 ) ) ;
#19493=CARTESIAN_POINT ( 'NONE',  ( 1.147381204815054234, 0.5174497483512505713, -7.899033294795724025 ) ) ;
#19527=DIRECTION ( 'NONE',  ( 8.672736310388503609E-16, 0.000000000000000000, 1.000000000000000000 ) ) ;
#19533=DIRECTION ( 'NONE',  ( -0.000000000000000000, -0.000000000000000000, 1.000000000000000000 ) ) ;
#19553=ORIENTED_EDGE ( 'NONE', *, *, #24186, .T. ) ;
#19615=ORIENTED_EDGE ( 'NONE', *, *, #14012, .T. ) ;
#19618=DIRECTION ( 'NONE',  ( 3.410983854926731543E-15, 1.734723475976805714E-15, -1.000000000000000000 ) ) ;
#19654=CARTESIAN_POINT ( 'NONE',  ( -5.772270645472310946, 14.99679128811752804, -2.402751277358635473 ) ) ;
#19657=LINE ( 'NONE', #22319, #23079 ) ;
#19684=DIRECTION ( 'NONE',  ( 1.734547262077700722E-15, 0.000000000000000000, 1.000000000000000000 ) ) ;
#19718=ORIENTED_EDGE ( 'NONE', *, *, #14697, .T. ) ;
#19724=DIRECTION ( 'NONE',  ( -1.000000000000000000, 0.000000000000000000, 0.000000000000000000 ) ) ;
#19739=AXIS2_PLACEMENT_3D ( 'NONE', #5445, #10457, #2969 ) ;
#19741=DIRECTION ( 'NONE',  ( 0.000000000000000000, 1.000000000000000000, 0.000000000000000000 ) ) ;
#19751=DIRECTION ( 'NONE',  ( -0.9896144216807901683, 0.000000000000000000, -0.1437473352845036190 ) ) ;
#19764=EDGE_CURVE ( 'NONE', #7632, #18687, #25071, .T. ) ;
#19774=DIRECTION ( 'NONE',  ( 0.1437473352845080599, 0.000000000000000000, -0.9896144216807893912 ) ) ;
#19779=CIRCLE ( 'NONE', #29927, 3.750000000000000444 ) ;
#19783=EDGE_CURVE ( 'NONE', #12125, #16462, #15976, .T. ) ;
#19848=CARTESIAN_POINT ( 'NONE',  ( 34.48223484310472031, 0.5000000000000000000, -2.999999999999997335 ) ) ;
#19903=DIRECTION ( 'NONE',  ( 0.03488359650710744914, -0.9989355049964836475, -0.03018263660036422935 ) ) ;
#19905=CARTESIAN_POINT ( 'NONE',  ( 1.075551320669168920, 0.000000000000000000, -7.404527507138932485 ) ) ;
#19925=ORIENTED_EDGE ( 'NONE', *, *, #31821, .F. ) ;
#19931=VECTOR ( 'NONE', #10290, 1000.000000000000000 ) ;
#19934=VECTOR ( 'NONE', #25323, 1000.000000000000227 ) ;
#19995=VECTOR ( 'NONE', #11502, 1000.000000000000114 ) ;
#20004=EDGE_CURVE ( 'NONE', #26351, #29995, #28677, .T. ) ;
#20012=DIRECTION ( 'NONE',  ( 1.000000000000000000, 1.387778780781445833E-14, 4.846230290920773249E-16 ) ) ;
#20025=ORIENTED_EDGE ( 'NONE', *, *, #17437, .F. ) ;
#20028=CARTESIAN_POINT ( 'NONE',  ( 12.44989959798868817, 0.000000000000000000, -2.482234843104710986 ) ) ;
#20033=EDGE_CURVE ( 'NONE', #6030, #9245, #30419, .T. ) ;
#20037=DIRECTION ( 'NONE',  ( 0.000000000000000000, 0.000000000000000000, 1.000000000000000000 ) ) ;
#20073=DIRECTION ( 'NONE',  ( 1.000000000000000000, -0.000000000000000000, 8.654346879536960414E-15 ) ) ;
#20092=ORIENTED_EDGE ( 'NONE', *, *, #9421, .T. ) ;
#20099=ORIENTED_EDGE ( 'NONE', *, *, #24305, .F. ) ;
#20120=CARTESIAN_POINT ( 'NONE',  ( 1.075551320669168476, 0.5000000000000000000, -7.404527507138929820 ) ) ;
#20140=ORIENTED_EDGE ( 'NONE', *, *, #18842, .T. ) ;
#20144=FACE_OUTER_BOUND ( 'NONE', #13725, .T. ) ;
#20150=DIRECTION ( 'NONE',  ( 0.000000000000000000, 0.000000000000000000, 1.000000000000000000 ) ) ;
#20156=DIRECTION ( 'NONE',  ( 1.000000000000000000, 0.000000000000000000, 3.469446951953611033E-15 ) ) ;
#20165=DIRECTION ( 'NONE',  ( 0.000000000000000000, 1.000000000000000000, 0.000000000000000000 ) ) ;
#20186=EDGE_CURVE ( 'NONE', #15174, #23664, #22649, .T. ) ;
#20228=ORIENTED_EDGE ( 'NONE', *, *, #17343, .F. ) ;
#20251=CARTESIAN_POINT ( 'NONE',  ( 33.81874022276149816, 19.50000000000000000, 1.818740222761736414 ) ) ;
#20259=DIRECTION ( 'NONE',  ( -1.000000000000000000, 0.000000000000000000, -3.469446951953611033E-15 ) ) ;
#20264=DIRECTION ( 'NONE',  ( 0.1437473352844943209, 0.000000000000000000, -0.9896144216807913896 ) ) ;
#20268=DIRECTION ( 'NONE',  ( 0.000000000000000000, 0.000000000000000000, 1.000000000000000000 ) ) ;
#20282=VERTEX_POINT ( 'NONE', #17445 ) ;
#20283=CARTESIAN_POINT ( 'NONE',  ( 0.000000000000000000, 20.00000000000000000, 6.818740222761507042 ) ) ;
#20284=ORIENTED_EDGE ( 'NONE', *, *, #22905, .F. ) ;
#20303=TOROIDAL_SURFACE ( 'NONE', #24546, 10.51776515689528502, 0.5000000000000000000 ) ;
#20326=ORIENTED_EDGE ( 'NONE', *, *, #17464, .F. ) ;
#20376=VECTOR ( 'NONE', #28429, 1000.000000000000227 ) ;
#20390=AXIS2_PLACEMENT_3D ( 'NONE', #12232, #21776, #26973 ) ;
#20412=FACE_OUTER_BOUND ( 'NONE', #21734, .T. ) ;
#20439=DIRECTION ( 'NONE',  ( 0.000000000000000000, 1.000000000000000000, 0.000000000000000000 ) ) ;
#20471=ORIENTED_EDGE ( 'NONE', *, *, #11850, .T. ) ;
#20480=CIRCLE ( 'NONE', #11390, 10.01776515689528502 ) ;
#20549=ORIENTED_EDGE ( 'NONE', *, *, #23193, .T. ) ;
#20586=ADVANCED_FACE ( 'NONE', ( #22693 ), #2620, .T. ) ;
#20630=DIRECTION ( 'NONE',  ( 0.03488359650710501358, -0.9989355049964838695, -0.03018263660036204360 ) ) ;
#20645=ORIENTED_EDGE ( 'NONE', *, *, #21448, .T. ) ;
#20668=VERTEX_POINT ( 'NONE', #598 ) ;
#20677=EDGE_LOOP ( 'NONE', ( #29470, #18326, #13511, #14514 ) ) ;
#20769=DIRECTION ( 'NONE',  ( 0.9896144216807900573, 0.000000000000000000, 0.1437473352845041463 ) ) ;
#20774=ORIENTED_EDGE ( 'NONE', *, *, #23360, .F. ) ;
#20799=DIRECTION ( 'NONE',  ( 0.000000000000000000, 8.673617379884035472E-16, -1.000000000000000000 ) ) ;
#20807=CARTESIAN_POINT ( 'NONE',  ( 34.99999999999999289, 0.5000000000000000000, 2.482234843104954791 ) ) ;
#20809=DIRECTION ( 'NONE',  ( 0.000000000000000000, 0.000000000000000000, 1.000000000000000000 ) ) ;
#20817=ORIENTED_EDGE ( 'NONE', *, *, #32827, .F. ) ;
#20823=CARTESIAN_POINT ( 'NONE',  ( 12.44989959798868817, 18.00000000000000355, 13.00000000000004441 ) ) ;
#20834=AXIS2_PLACEMENT_3D ( 'NONE', #445, #25868, #13141 ) ;
#20845=CARTESIAN_POINT ( 'NONE',  ( 5.175170698068133568, 0.5000000000000000000, 5.403836275575642389 ) ) ;
#20855=DIRECTION ( 'NONE',  ( 0.9896144216807899463, -0.000000000000000000, 0.1437473352845038410 ) ) ;
#20860=CIRCLE ( 'NONE', #17646, 0.4999999999999996114 ) ;
#20879=VERTEX_POINT ( 'NONE', #18108 ) ;
#20881=DIRECTION ( 'NONE',  ( 1.000000000000000000, -0.000000000000000000, 0.000000000000000000 ) ) ;
#20886=CIRCLE ( 'NONE', #29957, 0.4999999999999996114 ) ;
#20897=LINE ( 'NONE', #10194, #10720 ) ;
#20899=FACE_OUTER_BOUND ( 'NONE', #28875, .T. ) ;
#20981=CARTESIAN_POINT ( 'NONE',  ( 0.000000000000000000, 0.000000000000000000, 0.000000000000000000 ) ) ;
#20992=VECTOR ( 'NONE', #8533, 1000.000000000000227 ) ;
#21007=ORIENTED_EDGE ( 'NONE', *, *, #16539, .F. ) ;
#21026=CYLINDRICAL_SURFACE ( 'NONE', #30013, 0.5000000000000000000 ) ;
#21028=CYLINDRICAL_SURFACE ( 'NONE', #18259, 3.750000000000000444 ) ;
#21039=CIRCLE ( 'NONE', #29578, 7.318435636271054534 ) ;
#21061=CARTESIAN_POINT ( 'NONE',  ( 0.9801757370192284435, 20.00000000000000000, -6.747923662139671208 ) ) ;
#21065=EDGE_CURVE ( 'NONE', #4203, #29021, #3421, .T. ) ;
#21098=DIRECTION ( 'NONE',  ( 1.000000000000000000, 0.000000000000000000, -4.336808689942013792E-15 ) ) ;
#21099=CARTESIAN_POINT ( 'NONE',  ( -33.81874022276151948, 19.50000000000000000, -1.818740222761502601 ) ) ;
#21127=VERTEX_POINT ( 'NONE', #27459 ) ;
#21138=LINE ( 'NONE', #7595, #7141 ) ;
#21155=ORIENTED_EDGE ( 'NONE', *, *, #9644, .T. ) ;
#21166=ORIENTED_EDGE ( 'NONE', *, *, #5908, .T. ) ;
#21226=CARTESIAN_POINT ( 'NONE',  ( -33.81874022276151237, 19.50000000000000000, -1.818740222761502601 ) ) ;
#21247=DIRECTION ( 'NONE',  ( -0.03487826274237759705, -0.9987827659587180662, -0.03487826274237711827 ) ) ;
#21355=EDGE_CURVE ( 'NONE', #72, #22098, #31019, .T. ) ;
#21358=ORIENTED_EDGE ( 'NONE', *, *, #1221, .T. ) ;
#21375=AXIS2_PLACEMENT_3D ( 'NONE', #8165, #28716, #18371 ) ;
#21378=ORIENTED_EDGE ( 'NONE', *, *, #22165, .T. ) ;
#21407=AXIS2_PLACEMENT_3D ( 'NONE', #20251, #23093, #25768 ) ;
#21421=DIRECTION ( 'NONE',  ( 0.000000000000000000, -1.734723475976807094E-15, -1.000000000000000000 ) ) ;
#21448=EDGE_CURVE ( 'NONE', #30055, #27447, #26737, .T. ) ;
#21488=ORIENTED_EDGE ( 'NONE', *, *, #12649, .F. ) ;
#21495=DIRECTION ( 'NONE',  ( -0.9896144216807899463, 0.000000000000000000, -0.1437473352845038410 ) ) ;
#21501=DIRECTION ( 'NONE',  ( 0.000000000000000000, -1.000000000000000000, 0.000000000000000000 ) ) ;
#21506=DIRECTION ( 'NONE',  ( 0.000000000000000000, 0.03489949670250103164, -0.9993908270190957621 ) ) ;
#21524=ORIENTED_EDGE ( 'NONE', *, *, #551, .F. ) ;
#21536=CIRCLE ( 'NONE', #7118, 0.5000000000000000000 ) ;
#21548=CARTESIAN_POINT ( 'NONE',  ( 0.000000000000000000, 0.5000000000000000000, 0.000000000000000000 ) ) ;
#21549=CARTESIAN_POINT ( 'NONE',  ( -34.48223484310472031, 0.5000000000000000000, 2.552009564962238297 ) ) ;
#21558=ORIENTED_EDGE ( 'NONE', *, *, #18117, .F. ) ;
#21571=ORIENTED_EDGE ( 'NONE', *, *, #24977, .T. ) ;
#21579=ORIENTED_EDGE ( 'NONE', *, *, #32156, .F. ) ;
#21583=CARTESIAN_POINT ( 'NONE',  ( -32.99878091140236336, 0.000000000000000000, -0.9987809114023521451 ) ) ;
#21598=DIRECTION ( 'NONE',  ( 1.000000000000000000, 0.000000000000000000, 0.000000000000000000 ) ) ;
#21602=DIRECTION ( 'NONE',  ( 1.000000000000000000, -0.000000000000000000, 8.654346879536960414E-15 ) ) ;
#21649=DIRECTION ( 'NONE',  ( 0.000000000000000000, 1.000000000000000000, 0.000000000000000000 ) ) ;
#21662=LINE ( 'NONE', #31531, #31576 ) ;
#21677=ORIENTED_EDGE ( 'NONE', *, *, #23131, .T. ) ;
#21688=EDGE_LOOP ( 'NONE', ( #21677, #24013, #16928, #27318 ) ) ;
#21717=FACE_OUTER_BOUND ( 'NONE', #9665, .T. ) ;
#21734=EDGE_LOOP ( 'NONE', ( #21358, #6145, #7723, #13604 ) ) ;
#21749=DIRECTION ( 'NONE',  ( 0.000000000000000000, 0.000000000000000000, 1.000000000000000000 ) ) ;
#21757=ORIENTED_EDGE ( 'NONE', *, *, #6689, .F. ) ;
#21763=EDGE_CURVE ( 'NONE', #14980, #21865, #10153, .T. ) ;
#21773=CARTESIAN_POINT ( 'NONE',  ( -12.44989959798873791, 19.51744974835124680, -2.318435636271050537 ) ) ;
#21776=DIRECTION ( 'NONE',  ( 0.000000000000000000, 0.03489949670250105246, -0.9993908270190957621 ) ) ;
#21779=EDGE_LOOP ( 'NONE', ( #31900, #7050, #28909 ) ) ;
#21799=DIRECTION ( 'NONE',  ( 1.735780866781622650E-15, -0.000000000000000000, -1.000000000000000000 ) ) ;
#21802=ORIENTED_EDGE ( 'NONE', *, *, #13688, .T. ) ;
#21805=EDGE_CURVE ( 'NONE', #20282, #29098, #1073, .T. ) ;
#21816=DIRECTION ( 'NONE',  ( -1.000000000000000000, 0.000000000000000000, -8.654346879536960414E-15 ) ) ;
#21819=VERTEX_POINT ( 'NONE', #24504 ) ;
#21838=ADVANCED_FACE ( 'NONE', ( #14306 ), #22024, .F. ) ;
#21860=VECTOR ( 'NONE', #21495, 1000.000000000000227 ) ;
#21863=CARTESIAN_POINT ( 'NONE',  ( 33.81874022276149105, 19.51744974835125035, 2.318435636271284128 ) ) ;
#21865=VERTEX_POINT ( 'NONE', #412 ) ;
#21914=EDGE_CURVE ( 'NONE', #21819, #14956, #4296, .T. ) ;
#21930=VECTOR ( 'NONE', #22843, 1000.000000000000227 ) ;
#21935=ORIENTED_EDGE ( 'NONE', *, *, #5897, .T. ) ;
#21939=DIRECTION ( 'NONE',  ( 0.000000000000000000, 1.000000000000000000, 0.000000000000000000 ) ) ;
#21940=DIRECTION ( 'NONE',  ( 0.000000000000000000, -0.9993908270190956511, 0.03489949670250104552 ) ) ;
#21992=TOROIDAL_SURFACE ( 'NONE', #7589, 6.818740222761507042, 0.5000000000000000000 ) ;
#22019=ORIENTED_EDGE ( 'NONE', *, *, #11165, .F. ) ;
#22024=CYLINDRICAL_SURFACE ( 'NONE', #32588, 3.750000000000000444 ) ;
#22098=VERTEX_POINT ( 'NONE', #18608 ) ;
#22111=ORIENTED_EDGE ( 'NONE', *, *, #6195, .F. ) ;
#22118=DIRECTION ( 'NONE',  ( 3.471561733563245301E-15, 0.000000000000000000, -1.000000000000000000 ) ) ;
#22138=DIRECTION ( 'NONE',  ( 0.000000000000000000, 0.000000000000000000, -1.000000000000000000 ) ) ;
#22141=VERTEX_POINT ( 'NONE', #25446 ) ;
#22164=EDGE_CURVE ( 'NONE', #20879, #8919, #10050, .T. ) ;
#22165=EDGE_CURVE ( 'NONE', #15916, #27615, #59, .T. ) ;
#22168=CARTESIAN_POINT ( 'NONE',  ( -12.44989959798873791, 0.5000000000000000000, -2.982234843104710986 ) ) ;
#22194=CARTESIAN_POINT ( 'NONE',  ( 0.000000000000000000, 0.5000000000000000000, 7.482234843104714983 ) ) ;
#22195=EDGE_CURVE ( 'NONE', #3357, #8422, #2714, .T. ) ;
#22226=ORIENTED_EDGE ( 'NONE', *, *, #4340, .F. ) ;
#22252=FACE_OUTER_BOUND ( 'NONE', #27519, .T. ) ;
#22304=ORIENTED_EDGE ( 'NONE', *, *, #551, .T. ) ;
#22307=VERTEX_POINT ( 'NONE', #6198 ) ;
#22319=CARTESIAN_POINT ( 'NONE',  ( 34.99999999999999289, 0.000000000000000000, 0.9987809114025958390 ) ) ;
#22322=EDGE_LOOP ( 'NONE', ( #8212, #32474, #6219, #1367 ) ) ;
#22335=EDGE_CURVE ( 'NONE', #8396, #10028, #11778, .T. ) ;
#22345=DIRECTION ( 'NONE',  ( -1.000000000000000000, 0.000000000000000000, 0.000000000000000000 ) ) ;
#22351=DIRECTION ( 'NONE',  ( -0.9993908270190956511, 0.03489949670250350189, -1.734723475976808475E-15 ) ) ;
#22403=CARTESIAN_POINT ( 'NONE',  ( 34.98223484310472031, 0.5000000000000000000, -2.999999999999995559 ) ) ;
#22405=AXIS2_PLACEMENT_3D ( 'NONE', #10727, #13382, #25969 ) ;
#22427=ADVANCED_FACE ( 'NONE', ( #12043 ), #11693, .T. ) ;
#22448=AXIS2_PLACEMENT_3D ( 'NONE', #25047, #20073, #12349 ) ;
#22456=AXIS2_PLACEMENT_3D ( 'NONE', #3863, #19724, #6844 ) ;
#22474=EDGE_CURVE ( 'NONE', #974, #425, #8321, .T. ) ;
#22476=AXIS2_PLACEMENT_3D ( 'NONE', #16306, #11291, #1436 ) ;
#22530=CARTESIAN_POINT ( 'NONE',  ( -34.48223484310472031, 0.5000000000000000000, -2.482234843104710986 ) ) ;
#22554=CIRCLE ( 'NONE', #2277, 7.482234843104714983 ) ;
#22594=CIRCLE ( 'NONE', #10814, 7.318435636271054534 ) ;
#22606=CYLINDRICAL_SURFACE ( 'NONE', #31120, 0.5000000000000002220 ) ;
#22621=CIRCLE ( 'NONE', #8203, 0.4999999999999996669 ) ;
#22649=LINE ( 'NONE', #23139, #17045 ) ;
#22665=DIRECTION ( 'NONE',  ( -0.9896144216807905014, -0.000000000000000000, -0.1437473352845004826 ) ) ;
#22685=ORIENTED_EDGE ( 'NONE', *, *, #12617, .T. ) ;
#22693=FACE_OUTER_BOUND ( 'NONE', #24249, .T. ) ;
#22704=CARTESIAN_POINT ( 'NONE',  ( 0.000000000000000000, 19.51744974835125035, 0.000000000000000000 ) ) ;
#22710=CARTESIAN_POINT ( 'NONE',  ( 34.50091246256899780, -0.01740729335041252962, 3.000607876078799752 ) ) ;
#22718=LINE ( 'NONE', #32923, #25767 ) ;
#22749=LINE ( 'NONE', #12545, #14018 ) ;
#22752=VERTEX_POINT ( 'NONE', #19905 ) ;
#22754=ADVANCED_FACE ( 'NONE', ( #7195, #4837, #32944, #30422 ), #17890, .F. ) ;
#22767=CARTESIAN_POINT ( 'NONE',  ( -34.71233008869360503, 0.000000000000000000, 1.019564728980889567 ) ) ;
#22776=CARTESIAN_POINT ( 'NONE',  ( -12.44989959798873791, 18.00000000000000355, -12.99999999999999645 ) ) ;
#22803=ORIENTED_EDGE ( 'NONE', *, *, #13979, .T. ) ;
#22819=EDGE_CURVE ( 'NONE', #19157, #8703, #26235, .T. ) ;
#22830=VERTEX_POINT ( 'NONE', #8655 ) ;
#22841=DIRECTION ( 'NONE',  ( -1.000000000000000000, 0.000000000000000000, -3.469446951953611033E-15 ) ) ;
#22842=ORIENTED_EDGE ( 'NONE', *, *, #14697, .F. ) ;
#22843=DIRECTION ( 'NONE',  ( -0.9896144216807899463, 0.000000000000000000, -0.1437473352845035635 ) ) ;
#22850=DIRECTION ( 'NONE',  ( 0.000000000000000000, 1.000000000000000000, 0.000000000000000000 ) ) ;
#22857=SPHERICAL_SURFACE ( 'NONE', #8117, 0.5000000000000000000 ) ;
#22894=CARTESIAN_POINT ( 'NONE',  ( 0.000000000000000000, 0.5174497483512174867, 0.000000000000000000 ) ) ;
#22905=EDGE_CURVE ( 'NONE', #9377, #25215, #16492, .T. ) ;
#22913=ORIENTED_EDGE ( 'NONE', *, *, #12048, .F. ) ;
#22919=ORIENTED_EDGE ( 'NONE', *, *, #6497, .T. ) ;
#22930=LINE ( 'NONE', #30670, #7030 ) ;
#22964=SPHERICAL_SURFACE ( 'NONE', #19312, 0.5000000000000000000 ) ;
#22970=CIRCLE ( 'NONE', #21375, 0.5000000000000003331 ) ;
#22971=DIRECTION ( 'NONE',  ( -1.000000000000000000, 0.000000000000000000, -8.654346879536960414E-15 ) ) ;
#22992=ORIENTED_EDGE ( 'NONE', *, *, #11850, .F. ) ;
#23018=ORIENTED_EDGE ( 'NONE', *, *, #28333, .F. ) ;
#23061=DIRECTION ( 'NONE',  ( 0.000000000000000000, 1.000000000000000000, 0.000000000000000000 ) ) ;
#23076=CARTESIAN_POINT ( 'NONE',  ( -35.00000000000000000, 0.000000000000000000, 3.000000000000004441 ) ) ;
#23079=VECTOR ( 'NONE', #17622, 1000.000000000000000 ) ;
#23085=FACE_OUTER_BOUND ( 'NONE', #1219, .T. ) ;
#23091=ORIENTED_EDGE ( 'NONE', *, *, #129, .F. ) ;
#23093=DIRECTION ( 'NONE',  ( 1.000000000000000000, -0.000000000000000000, 1.388624693425297489E-14 ) ) ;
#23104=DIRECTION ( 'NONE',  ( 0.9896144216807907235, -1.385833989420258499E-14, 0.1437473352844997332 ) ) ;
#23108=CIRCLE ( 'NONE', #8679, 7.318435636271054534 ) ;
#23122=CIRCLE ( 'NONE', #31670, 3.750000000000000444 ) ;
#23131=EDGE_CURVE ( 'NONE', #24949, #8736, #20886, .T. ) ;
#23132=PRODUCT_DEFINITION ( 'UNKNOWN', '', #12467, #12502 ) ;
#23139=CARTESIAN_POINT ( 'NONE',  ( -12.44989959798873436, 19.51744974835125035, -2.318435636271050537 ) ) ;
#23164=VECTOR ( 'NONE', #15614, 1000.000000000000114 ) ;
#23173=DIRECTION ( 'NONE',  ( 1.000000000000000000, 0.000000000000000000, 0.000000000000000000 ) ) ;
#23193=EDGE_CURVE ( 'NONE', #24814, #30219, #5945, .T. ) ;
#23198=EDGE_CURVE ( 'NONE', #29383, #425, #2809, .T. ) ;
#23201=CARTESIAN_POINT ( 'NONE',  ( 0.000000000000000000, 0.000000000000000000, 8.000000000000000000 ) ) ;
#23207=CARTESIAN_POINT ( 'NONE',  ( -34.98223484310472031, 0.5000000000000000000, 3.000000000000004441 ) ) ;
#23218=DIRECTION ( 'NONE',  ( 0.1437473352845080599, 0.000000000000000000, -0.9896144216807893912 ) ) ;
#23230=CARTESIAN_POINT ( 'NONE',  ( 0.000000000000000000, 0.5000000000000000000, 0.000000000000000000 ) ) ;
#23254=CARTESIAN_POINT ( 'NONE',  ( -12.44989959798873791, 19.50000000000000000, -12.99999999999999645 ) ) ;
#23258=EDGE_LOOP ( 'NONE', ( #30295, #22111, #1334, #22685 ) ) ;
#23282=DIRECTION ( 'NONE',  ( -1.000000000000000000, 0.000000000000000000, 0.000000000000000000 ) ) ;
#23283=LINE ( 'NONE', #10558, #20992 ) ;
#23327=ADVANCED_FACE ( 'NONE', ( #16807 ), #14274, .T. ) ;
#23348=DIRECTION ( 'NONE',  ( 0.03488359650710490256, 0.9989355049964836475, -0.03018263660036206442 ) ) ;
#23360=EDGE_CURVE ( 'NONE', #23664, #7166, #17705, .T. ) ;
#23362=EDGE_CURVE ( 'NONE', #6075, #4203, #1152, .T. ) ;
#23377=VERTEX_POINT ( 'NONE', #17311 ) ;
#23439=ORIENTED_EDGE ( 'NONE', *, *, #82, .T. ) ;
#23448=ORIENTED_EDGE ( 'NONE', *, *, #4266, .T. ) ;
#23515=EDGE_LOOP ( 'NONE', ( #18146, #25397, #27492, #14055 ) ) ;
#23517=ADVANCED_FACE ( 'NONE', ( #28658 ), #22964, .T. ) ;
#23521=AXIS2_PLACEMENT_3D ( 'NONE', #31138, #8224, #16229 ) ;
#23542=DIRECTION ( 'NONE',  ( 0.000000000000000000, 0.000000000000000000, 1.000000000000000000 ) ) ;
#23547=AXIS2_PLACEMENT_3D ( 'NONE', #28236, #20881, #15361 ) ;
#23561=VERTEX_POINT ( 'NONE', #29146 ) ;
#23562=CARTESIAN_POINT ( 'NONE',  ( 5.323856294847530535, 1.496472198897159434, 3.277537277937063731 ) ) ;
#23595=TOROIDAL_SURFACE ( 'NONE', #3335, 6.818740222761507042, 0.5000000000000000000 ) ;
#23614=EDGE_LOOP ( 'NONE', ( #5594, #21935, #19553, #30548 ) ) ;
#23622=LINE ( 'NONE', #18605, #9559 ) ;
#23646=AXIS2_PLACEMENT_3D ( 'NONE', #13157, #16158, #10820 ) ;
#23664=VERTEX_POINT ( 'NONE', #21773 ) ;
#23670=DIRECTION ( 'NONE',  ( 0.1437473352845043406, 0.000000000000000000, -0.9896144216807899463 ) ) ;
#23725=CARTESIAN_POINT ( 'NONE',  ( -33.81874022276151237, 19.50000000000000000, 1.977928362984241017 ) ) ;
#23745=FACE_OUTER_BOUND ( 'NONE', #9786, .T. ) ;
#23774=DIRECTION ( 'NONE',  ( 0.000000000000000000, 0.000000000000000000, 1.000000000000000000 ) ) ;
#23785=VERTEX_POINT ( 'NONE', #4571 ) ;
#23800=CARTESIAN_POINT ( 'NONE',  ( 0.000000000000000000, 0.000000000000000000, 7.482234843104714983 ) ) ;
#23823=DIRECTION ( 'NONE',  ( 0.000000000000000000, 0.03489949670250105246, -0.9993908270190957621 ) ) ;
#23838=LINE ( 'NONE', #23207, #9707 ) ;
#23870=DIRECTION ( 'NONE',  ( 1.000000000000000000, 0.000000000000000000, 0.000000000000000000 ) ) ;
#23887=ORIENTED_EDGE ( 'NONE', *, *, #11632, .T. ) ;
#23893=DIRECTION ( 'NONE',  ( -0.000000000000000000, -1.000000000000000000, -0.000000000000000000 ) ) ;
#23907=DIRECTION ( 'NONE',  ( -0.6916610887771522664, 0.000000000000000000, -0.7222222222222217658 ) ) ;
#23924=LINE ( 'NONE', #8544, #8058 ) ;
#23975=DIRECTION ( 'NONE',  ( 1.000000000000000000, 1.387778780781445833E-14, 4.846230290920773249E-16 ) ) ;
#23984=CARTESIAN_POINT ( 'NONE',  ( -34.49361350329746756, 0.1741578047003206897, -2.493613503297456013 ) ) ;
#23985=DIRECTION ( 'NONE',  ( 3.471561733563245301E-15, 0.000000000000000000, -1.000000000000000000 ) ) ;
#23988=ORIENTED_EDGE ( 'NONE', *, *, #15570, .F. ) ;
#24003=DIRECTION ( 'NONE',  ( 0.000000000000000000, 0.000000000000000000, 1.000000000000000000 ) ) ;
#24010=AXIS2_PLACEMENT_3D ( 'NONE', #24012, #11817, #19527 ) ;
#24012=CARTESIAN_POINT ( 'NONE',  ( -12.44989959798873791, 0.000000000000000000, -12.99999999999999645 ) ) ;
#24013=ORIENTED_EDGE ( 'NONE', *, *, #10601, .F. ) ;
#24068=CARTESIAN_POINT ( 'NONE',  ( 0.000000000000000000, 18.00000000000000355, 0.000000000000000000 ) ) ;
#24076=ADVANCED_FACE ( 'NONE', ( #25695 ), #22857, .T. ) ;
#24085=B_SPLINE_CURVE_WITH_KNOTS ( 'NONE', 3,
 ( #6926, #19654, #24648, #12121, #9093, #6617, #14785, #29691 ),
 .UNSPECIFIED., .F., .F.,
 ( 4, 2, 2, 4 ),
 ( 9.034501660022746213E-05, 0.009114482626497340256, 0.01362655143144589527, 0.01813862023639444682 ),
 .UNSPECIFIED. ) ;
#24088=ORIENTED_EDGE ( 'NONE', *, *, #18842, .F. ) ;
#24102=DIRECTION ( 'NONE',  ( -0.03487826274237469659, -0.9987827659587182882, -0.03487826274237469659 ) ) ;
#24138=DIRECTION ( 'NONE',  ( -0.03488359650710499277, 0.9989355049964836475, 0.03018263660036203666 ) ) ;
#24152=DIRECTION ( 'NONE',  ( 1.040834085586084257E-14, 0.000000000000000000, -1.000000000000000000 ) ) ;
#24186=EDGE_CURVE ( 'NONE', #21865, #9415, #32912, .T. ) ;
#24196=DIRECTION ( 'NONE',  ( 0.000000000000000000, 1.000000000000000000, 0.000000000000000000 ) ) ;
#24216=CIRCLE ( 'NONE', #14039, 0.5000000000000004441 ) ;
#24233=CARTESIAN_POINT ( 'NONE',  ( 5.509727295071394693, 5.993169562190667321, 2.952988490976601099 ) ) ;
#24240=DIRECTION ( 'NONE',  ( 3.469446951953478110E-15, -0.000000000000000000, -1.000000000000000000 ) ) ;
#24249=EDGE_LOOP ( 'NONE', ( #14361, #253, #22992, #24671 ) ) ;
#24257=ADVANCED_FACE ( 'NONE', ( #13636 ), #21028, .F. ) ;
#24263=SPHERICAL_SURFACE ( 'NONE', #19415, 0.5000000000000000000 ) ;
#24264=EDGE_CURVE ( 'NONE', #12815, #27372, #23838, .T. ) ;
#24279=ORIENTED_EDGE ( 'NONE', *, *, #26933, .F. ) ;
#24297=CARTESIAN_POINT ( 'NONE',  ( -5.521001242456725855, 0.4999999999999998890, -5.764947386686739783 ) ) ;
#24305=EDGE_CURVE ( 'NONE', #16462, #22307, #16645, .T. ) ;
#24314=EDGE_CURVE ( 'NONE', #13727, #22830, #18652, .T. ) ;
#24321=CARTESIAN_POINT ( 'NONE',  ( -12.44989959798873791, 19.50000000000000000, -1.818740222761502601 ) ) ;
#24325=EDGE_CURVE ( 'NONE', #23377, #8422, #28552, .T. ) ;
#24331=CARTESIAN_POINT ( 'NONE',  ( 2.598264985223430301, 0.000000000000000000, -5.684322216989628807 ) ) ;
#24341=ORIENTED_EDGE ( 'NONE', *, *, #15570, .T. ) ;
#24347=VERTEX_POINT ( 'NONE', #22168 ) ;
#24352=LINE ( 'NONE', #11001, #6492 ) ;
#24357=ORIENTED_EDGE ( 'NONE', *, *, #31420, .F. ) ;
#24374=CARTESIAN_POINT ( 'NONE',  ( 12.96639998074314271, 0.000000000000000000, 9.444203806868394224 ) ) ;
#24393=CYLINDRICAL_SURFACE ( 'NONE', #4319, 0.5000000000000002220 ) ;
#24422=ORIENTED_EDGE ( 'NONE', *, *, #32156, .T. ) ;
#24427=EDGE_LOOP ( 'NONE', ( #10259, #3570, #23448, #15295 ) ) ;
#24438=DIRECTION ( 'NONE',  ( -0.03489949670250104552, 0.9993908270190956511, 0.000000000000000000 ) ) ;
#24445=ORIENTED_EDGE ( 'NONE', *, *, #28744, .F. ) ;
#24447=ADVANCED_FACE ( 'NONE', ( #3623 ), #9282, .F. ) ;
#24471=EDGE_CURVE ( 'NONE', #10785, #9954, #13783, .T. ) ;
#24485=LINE ( 'NONE', #29702, #2662 ) ;
#24504=CARTESIAN_POINT ( 'NONE',  ( -1.147424988311422256, 0.5000000000000000000, 7.899334717979326292 ) ) ;
#24523=( BOUNDED_CURVE ( )  B_SPLINE_CURVE ( 3, ( #24331, #11620, #32024, #19323 ),
 .UNSPECIFIED., .F., .F. ) 
 B_SPLINE_CURVE_WITH_KNOTS ( ( 4, 4 ),
 ( 0.2844899013887131067, 0.5370275574894030068 ),
 .UNSPECIFIED. ) 
 CURVE ( )  GEOMETRIC_REPRESENTATION_ITEM ( )  RATIONAL_B_SPLINE_CURVE ( ( 1.000000000000000000, 0.9946924518608444288, 0.9946924518608444288, 1.000000000000000000 ) ) 
 REPRESENTATION_ITEM ( '' )  );
#24546=AXIS2_PLACEMENT_3D ( 'NONE', #26269, #20439, #15392 ) ;
#24548=EDGE_LOOP ( 'NONE', ( #21579, #6152, #22019, #28037 ) ) ;
#24551=EDGE_CURVE ( 'NONE', #29952, #24347, #16155, .T. ) ;
#24554=ORIENTED_EDGE ( 'NONE', *, *, #2801, .F. ) ;
#24569=FACE_OUTER_BOUND ( 'NONE', #15304, .T. ) ;
#24616=AXIS2_PLACEMENT_3D ( 'NONE', #13092, #20630, #30838 ) ;
#24637=DIRECTION ( 'NONE',  ( 3.471561733563293027E-15, 0.000000000000000000, -1.000000000000000000 ) ) ;
#24642=CARTESIAN_POINT ( 'NONE',  ( -12.44989959798873791, 19.51744974835125035, -12.99999999999999645 ) ) ;
#24648=CARTESIAN_POINT ( 'NONE',  ( -5.699736881468957961, 11.99440202994180993, -2.572806452144713152 ) ) ;
#24671=ORIENTED_EDGE ( 'NONE', *, *, #24325, .F. ) ;
#24712=ORIENTED_EDGE ( 'NONE', *, *, #7278, .T. ) ;
#24724=AXIS2_PLACEMENT_3D ( 'NONE', #10231, #7895, #10721 ) ;
#24737=CARTESIAN_POINT ( 'NONE',  ( 33.81874022276150527, 19.50000000000000000, -1.977928362984232802 ) ) ;
#24777=DIRECTION ( 'NONE',  ( 1.000000000000000000, 0.000000000000000000, 0.000000000000000000 ) ) ;
#24803=CYLINDRICAL_SURFACE ( 'NONE', #9277, 0.5000000000000000000 ) ;
#24814=VERTEX_POINT ( 'NONE', #1733 ) ;
#24848=FACE_OUTER_BOUND ( 'NONE', #4632, .T. ) ;
#24902=DIRECTION ( 'NONE',  ( 0.03488359650710500665, -0.9989355049964836475, -0.03018263660036204013 ) ) ;
#24917=EDGE_CURVE ( 'NONE', #7166, #10028, #32496, .T. ) ;
#24926=LINE ( 'NONE', #14370, #32203 ) ;
#24929=ORIENTED_EDGE ( 'NONE', *, *, #10601, .T. ) ;
#24938=CARTESIAN_POINT ( 'NONE',  ( 34.98223484310469900, 0.5000000000000000000, 2.482234843104951239 ) ) ;
#24947=PLANE ( 'NONE',  #5450 ) ;
#24949=VERTEX_POINT ( 'NONE', #9405 ) ;
#24965=VERTEX_POINT ( 'NONE', #14753 ) ;
#24975=CARTESIAN_POINT ( 'NONE',  ( 33.81874022276151237, 19.50000000000000000, -1.977928362984232802 ) ) ;
#24977=EDGE_CURVE ( 'NONE', #20879, #6075, #25231, .T. ) ;
#25001=CARTESIAN_POINT ( 'NONE',  ( -34.57258968893669504, -0.01303574654798582769, 3.062543865805540388 ) ) ;
#25031=EDGE_LOOP ( 'NONE', ( #27346, #19718, #26772, #1579 ) ) ;
#25047=CARTESIAN_POINT ( 'NONE',  ( 12.44989959798878587, 19.50000000000000000, 1.818740222761551451 ) ) ;
#25071=CIRCLE ( 'NONE', #10666, 0.4999999999999997780 ) ;
#25074=( NAMED_UNIT ( * ) PLANE_ANGLE_UNIT ( ) SI_UNIT ( $, .RADIAN. ) );
#25082=EDGE_LOOP ( 'NONE', ( #1709, #14214, #24712, #24357 ) ) ;
#25086=FACE_OUTER_BOUND ( 'NONE', #30000, .T. ) ;
#25103=CARTESIAN_POINT ( 'NONE',  ( 34.99740252253902639, 0.5174497483512504603, -2.982117921349399570 ) ) ;
#25108=CARTESIAN_POINT ( 'NONE',  ( 4.592425496802574958E-16, 0.000000000000000000, 3.750000000000000444 ) ) ;
#25118=EDGE_CURVE ( 'NONE', #22307, #17664, #16702, .T. ) ;
#25123=EDGE_LOOP ( 'NONE', ( #363, #3742, #1001, #25455 ) ) ;
#25128=DIRECTION ( 'NONE',  ( 1.735780866781622650E-15, -0.000000000000000000, -1.000000000000000000 ) ) ;
#25158=DIRECTION ( 'NONE',  ( 0.000000000000000000, -0.000000000000000000, 1.000000000000000000 ) ) ;
#25161=CARTESIAN_POINT ( 'NONE',  ( -1.147381204815053790, 0.5174497483512505713, 7.899033294795724025 ) ) ;
#25188=CARTESIAN_POINT ( 'NONE',  ( -33.81874022276151237, 19.50000000000000000, 1.977928362984241017 ) ) ;
#25190=EDGE_CURVE ( 'NONE', #22098, #15174, #7651, .T. ) ;
#25201=VECTOR ( 'NONE', #5479, 1000.000000000000227 ) ;
#25215=VERTEX_POINT ( 'NONE', #26599 ) ;
#25231=CIRCLE ( 'NONE', #9204, 0.4999999999999996669 ) ;
#25239=DIRECTION ( 'NONE',  ( 0.000000000000000000, 1.000000000000000000, 0.000000000000000000 ) ) ;
#25250=EDGE_CURVE ( 'NONE', #27372, #28120, #6047, .T. ) ;
#25323=DIRECTION ( 'NONE',  ( 0.9896144216807899463, -0.000000000000000000, 0.1437473352845038410 ) ) ;
#25344=CARTESIAN_POINT ( 'NONE',  ( -33.81874022276151237, 19.50000000000000000, 13.00000000000004441 ) ) ;
#25397=ORIENTED_EDGE ( 'NONE', *, *, #31821, .T. ) ;
#25413=DIRECTION ( 'NONE',  ( 0.000000000000000000, 1.000000000000000000, 0.000000000000000000 ) ) ;
#25446=CARTESIAN_POINT ( 'NONE',  ( 5.520790571833095406, 0.5174497483512504603, 5.764727407554761207 ) ) ;
#25455=ORIENTED_EDGE ( 'NONE', *, *, #20186, .F. ) ;
#25465=ORIENTED_EDGE ( 'NONE', *, *, #11618, .T. ) ;
#25468=DIRECTION ( 'NONE',  ( 0.9896144216807899463, -0.000000000000000000, 0.1437473352845038410 ) ) ;
#25474=DIRECTION ( 'NONE',  ( -0.6916610887771488247, 0.000000000000000000, -0.7222222222222250965 ) ) ;
#25482=EDGE_CURVE ( 'NONE', #8736, #72, #22749, .T. ) ;
#25496=DIRECTION ( 'NONE',  ( 1.387778780781445676E-14, -1.000000000000000000, 0.000000000000000000 ) ) ;
#25527=LINE ( 'NONE', #131, #11359 ) ;
#25558=ORIENTED_EDGE ( 'NONE', *, *, #17464, .T. ) ;
#25560=DIRECTION ( 'NONE',  ( -0.000000000000000000, -1.000000000000000000, -0.000000000000000000 ) ) ;
#25592=AXIS2_PLACEMENT_3D ( 'NONE', #24321, #26826, #3948 ) ;
#25601=DIRECTION ( 'NONE',  ( 0.000000000000000000, 0.000000000000000000, 1.000000000000000000 ) ) ;
#25628=DIRECTION ( 'NONE',  ( 1.000000000000000000, -0.000000000000000000, -0.000000000000000000 ) ) ;
#25633=FACE_OUTER_BOUND ( 'NONE', #1655, .T. ) ;
#25659=DIRECTION ( 'NONE',  ( 4.163336342344337027E-14, 0.03489949670250347413, 0.9993908270190957621 ) ) ;
#25664=B_SPLINE_CURVE_WITH_KNOTS ( 'NONE', 3,
 ( #18712, #28914, #16519, #14022, #24233, #8213, #23562, #686 ),
 .UNSPECIFIED., .F., .F.,
 ( 4, 2, 2, 4 ),
 ( 9.034501660023095868E-05, 0.009114482626497338522, 0.01362655143144589354, 0.01813862023639444682 ),
 .UNSPECIFIED. ) ;
#25673=CARTESIAN_POINT ( 'NONE',  ( 33.81874022276145553, 19.50000000000000000, 13.00000000000011902 ) ) ;
#25679=CYLINDRICAL_SURFACE ( 'NONE', #11881, 0.5000000000000004441 ) ;
#25695=FACE_OUTER_BOUND ( 'NONE', #31493, .T. ) ;
#25756=LINE ( 'NONE', #18218, #20376 ) ;
#25758=AXIS2_PLACEMENT_3D ( 'NONE', #4942, #276, #17461 ) ;
#25762=ORIENTED_EDGE ( 'NONE', *, *, #13979, .F. ) ;
#25767=VECTOR ( 'NONE', #15184, 1000.000000000000000 ) ;
#25768=DIRECTION ( 'NONE',  ( 1.387778780781445676E-14, 0.000000000000000000, -1.000000000000000000 ) ) ;
#25799=AXIS2_PLACEMENT_3D ( 'NONE', #23254, #14, #357 ) ;
#25850=CARTESIAN_POINT ( 'NONE',  ( 0.000000000000000000, 0.000000000000000000, -3.750000000000000444 ) ) ;
#25868=DIRECTION ( 'NONE',  ( -0.9896144216807905014, -0.000000000000000000, -0.1437473352845003161 ) ) ;
#25882=UNCERTAINTY_MEASURE_WITH_UNIT (LENGTH_MEASURE( 1.000000000000000082E-05 ), #7029, 'distance_accuracy_value', 'NONE');
#25894=FACE_OUTER_BOUND ( 'NONE', #25082, .T. ) ;
#25914=EDGE_CURVE ( 'NONE', #72, #15174, #1261, .T. ) ;
#25943=CARTESIAN_POINT ( 'NONE',  ( -33.81874022276151237, 19.50000000000000000, -1.818740222761503045 ) ) ;
#25954=DIRECTION ( 'NONE',  ( 0.000000000000000000, -0.03489949670250135777, -0.9993908270190957621 ) ) ;
#25964=CARTESIAN_POINT ( 'NONE',  ( -12.44989959798873791, 0.000000000000000000, -12.99999999999999645 ) ) ;
#25969=DIRECTION ( 'NONE',  ( 0.1437473352845037022, 0.000000000000000000, -0.9896144216807900573 ) ) ;
#25984=ORIENTED_EDGE ( 'NONE', *, *, #26141, .T. ) ;
#25989=ADVANCED_FACE ( 'NONE', ( #11870 ), #9507, .T. ) ;
#26025=EDGE_CURVE ( 'NONE', #27447, #13727, #11538, .T. ) ;
#26031=DIRECTION ( 'NONE',  ( 8.678904333908113252E-16, 0.000000000000000000, -1.000000000000000000 ) ) ;
#26089=EDGE_LOOP ( 'NONE', ( #31813, #1986, #16903, #14645, #673 ) ) ;
#26098=EDGE_CURVE ( 'NONE', #12815, #28083, #28492, .T. ) ;
#26141=EDGE_CURVE ( 'NONE', #24949, #21127, #22621, .T. ) ;
#26224=DIRECTION ( 'NONE',  ( -0.9896144216807899463, 0.000000000000000000, -0.1437473352845038410 ) ) ;
#26230=DIRECTION ( 'NONE',  ( 0.000000000000000000, 0.000000000000000000, 1.000000000000000000 ) ) ;
#26235=CIRCLE ( 'NONE', #28353, 3.750000000000000444 ) ;
#26269=CARTESIAN_POINT ( 'NONE',  ( 12.44989959798868817, 0.5000000000000000000, 13.00000000000004441 ) ) ;
#26289=CIRCLE ( 'NONE', #16130, 6.250000000000000000 ) ;
#26293=AXIS2_PLACEMENT_3D ( 'NONE', #8157, #18363, #15837 ) ;
#26299=DIRECTION ( 'NONE',  ( -0.9896144216807899463, 8.678901113238559347E-19, -0.1437473352845035635 ) ) ;
#26303=ORIENTED_EDGE ( 'NONE', *, *, #14649, .T. ) ;
#26315=AXIS2_PLACEMENT_3D ( 'NONE', #18250, #28465, #17934 ) ;
#26319=CONICAL_SURFACE ( 'NONE', #2314, 10.00000000000000355, 0.03490658503988666728 ) ;
#26341=ORIENTED_EDGE ( 'NONE', *, *, #17343, .T. ) ;
#26351=VERTEX_POINT ( 'NONE', #3818 ) ;
#26368=CARTESIAN_POINT ( 'NONE',  ( 12.44989959798878587, 20.00000000000000000, 1.818740222761551451 ) ) ;
#26401=ORIENTED_EDGE ( 'NONE', *, *, #2603, .T. ) ;
#26443=EDGE_LOOP ( 'NONE', ( #17011, #15687, #12805, #31136 ) ) ;
#26479=CARTESIAN_POINT ( 'NONE',  ( 34.98193025661424826, 0.5174497483512506824, 2.482234843104951239 ) ) ;
#26487=ORIENTED_EDGE ( 'NONE', *, *, #15212, .T. ) ;
#26561=LINE ( 'NONE', #16500, #28981 ) ;
#26567=DIRECTION ( 'NONE',  ( 0.03487826274237457863, -0.9987827659587181772, 0.03487826274237498803 ) ) ;
#26584=CARTESIAN_POINT ( 'NONE',  ( 32.37020706055090358, 18.00000000000000355, -3.000000000000004885 ) ) ;
#26599=CARTESIAN_POINT ( 'NONE',  ( 12.44989959798877699, 0.5174497483512504603, 2.981930256614307329 ) ) ;
#26624=DIRECTION ( 'NONE',  ( 0.1436597682917715446, 0.03489949670250103858, -0.9890115753135888532 ) ) ;
#26665=FACE_OUTER_BOUND ( 'NONE', #21688, .T. ) ;
#26695=FACE_OUTER_BOUND ( 'NONE', #23614, .T. ) ;
#26707=EDGE_CURVE ( 'NONE', #26351, #32786, #3364, .T. ) ;
#26720=ADVANCED_FACE ( 'NONE', ( #26665 ), #3777, .T. ) ;
#26737=LINE ( 'NONE', #26584, #5891 ) ;
#26759=DIRECTION ( 'NONE',  ( 0.000000000000000000, 0.000000000000000000, -1.000000000000000000 ) ) ;
#26766=EDGE_LOOP ( 'NONE', ( #5089, #14892, #5802, #13684, #13315 ) ) ;
#26772=ORIENTED_EDGE ( 'NONE', *, *, #12326, .T. ) ;
#26826=DIRECTION ( 'NONE',  ( 1.000000000000000000, 0.000000000000000000, 0.000000000000000000 ) ) ;
#26861=ORIENTED_EDGE ( 'NONE', *, *, #6785, .T. ) ;
#26879=DIRECTION ( 'NONE',  ( 0.03487826274237464802, -0.9987827659587182882, 0.03487826274237493945 ) ) ;
#26895=AXIS2_PLACEMENT_3D ( 'NONE', #2557, #12724, #25954 ) ;
#26900=AXIS2_PLACEMENT_3D ( 'NONE', #30359, #5117, #25659 ) ;
#26914=VERTEX_POINT ( 'NONE', #13080 ) ;
#26930=ORIENTED_EDGE ( 'NONE', *, *, #1166, .F. ) ;
#26933=EDGE_CURVE ( 'NONE', #13010, #23377, #31153, .T. ) ;
#26946=DIRECTION ( 'NONE',  ( 0.7222222222222246524, 0.000000000000000000, -0.6916610887771492688 ) ) ;
#26973=DIRECTION ( 'NONE',  ( 0.000000000000000000, 0.9993908270190956511, 0.03489949670250104552 ) ) ;
#26975=EDGE_LOOP ( 'NONE', ( #8108, #14378, #18905 ) ) ;
#26984=EDGE_CURVE ( 'NONE', #15916, #425, #2313, .T. ) ;
#27019=VERTEX_POINT ( 'NONE', #29432 ) ;
#27042=LINE ( 'NONE', #16995, #19995 ) ;
#27053=DIRECTION ( 'NONE',  ( -0.9896144216807899463, 0.000000000000000000, -0.1437473352845035635 ) ) ;
#27059=VERTEX_POINT ( 'NONE', #8191 ) ;
#27119=FACE_OUTER_BOUND ( 'NONE', #9510, .T. ) ;
#27131=ORIENTED_EDGE ( 'NONE', *, *, #4851, .F. ) ;
#27139=ORIENTED_EDGE ( 'NONE', *, *, #24917, .F. ) ;
#27149=CARTESIAN_POINT ( 'NONE',  ( -34.55410851074696410, 0.5000000000000000000, 3.046816775802633881 ) ) ;
#27172=VERTEX_POINT ( 'NONE', #3350 ) ;
#27177=DIRECTION ( 'NONE',  ( -1.387778780781445676E-14, 0.000000000000000000, 1.000000000000000000 ) ) ;
#27178=EDGE_CURVE ( 'NONE', #28120, #28083, #26561, .T. ) ;
#27223=ORIENTED_EDGE ( 'NONE', *, *, #6785, .F. ) ;
#27231=DIRECTION ( 'NONE',  ( -0.9896144216807901683, 0.000000000000000000, -0.1437473352845036190 ) ) ;
#27265=CIRCLE ( 'NONE', #11253, 11.18125977723849296 ) ;
#27267=CIRCLE ( 'NONE', #21407, 0.5000000000000000000 ) ;
#27269=CIRCLE ( 'NONE', #5489, 0.5000000000000004441 ) ;
#27306=TOROIDAL_SURFACE ( 'NONE', #29994, 11.18125977723849296, 0.5000000000000000000 ) ;
#27318=ORIENTED_EDGE ( 'NONE', *, *, #1221, .F. ) ;
#27327=AXIS2_PLACEMENT_3D ( 'NONE', #28725, #10848, #8483 ) ;
#27346=ORIENTED_EDGE ( 'NONE', *, *, #5441, .T. ) ;
#27350=AXIS2_PLACEMENT_3D ( 'NONE', #20845, #28701, #30898 ) ;
#27356=AXIS2_PLACEMENT_3D ( 'NONE', #1546, #11236, #11726 ) ;
#27371=DIRECTION ( 'NONE',  ( 0.1437473352845032581, 0.000000000000000000, -0.9896144216807900573 ) ) ;
#27372=VERTEX_POINT ( 'NONE', #12951 ) ;
#27373=VECTOR ( 'NONE', #19533, 1000.000000000000000 ) ;
#27398=ORIENTED_EDGE ( 'NONE', *, *, #30932, .F. ) ;
#27412=ADVANCED_FACE ( 'NONE', ( #18305 ), #2851, .T. ) ;
#27442=ORIENTED_EDGE ( 'NONE', *, *, #30932, .T. ) ;
#27447=VERTEX_POINT ( 'NONE', #18473 ) ;
#27455=ORIENTED_EDGE ( 'NONE', *, *, #9846, .F. ) ;
#27459=CARTESIAN_POINT ( 'NONE',  ( -33.81874022276151237, 20.00000000000000000, 1.977928362984239019 ) ) ;
#27470=DIRECTION ( 'NONE',  ( 1.000000000000000000, 0.000000000000000000, 0.000000000000000000 ) ) ;
#27471=CARTESIAN_POINT ( 'NONE',  ( 34.48223484310472031, 0.5000000000000000000, -2.552009564962230304 ) ) ;
#27479=ORIENTED_EDGE ( 'NONE', *, *, #21805, .F. ) ;
#27492=ORIENTED_EDGE ( 'NONE', *, *, #2532, .F. ) ;
#27495=CARTESIAN_POINT ( 'NONE',  ( 15.11750262208148499, 0.000000000000000000, -5.364851207409463640 ) ) ;
#27519=EDGE_LOOP ( 'NONE', ( #29500, #10211, #9202, #3192 ) ) ;
#27541=CARTESIAN_POINT ( 'NONE',  ( 12.44989959798868817, 0.000000000000000000, 13.00000000000004441 ) ) ;
#27593=EDGE_CURVE ( 'NONE', #23377, #6237, #194, .T. ) ;
#27615=VERTEX_POINT ( 'NONE', #8906 ) ;
#27659=LINE ( 'NONE', #1774, #32103 ) ;
#27661=DIRECTION ( 'NONE',  ( 0.000000000000000000, 0.000000000000000000, 1.000000000000000000 ) ) ;
#27668=CARTESIAN_POINT ( 'NONE',  ( -34.48223484310472742, 0.5000000000000000000, -2.482234843104710986 ) ) ;
#27670=ORIENTED_EDGE ( 'NONE', *, *, #24471, .T. ) ;
#27686=DIRECTION ( 'NONE',  ( 1.000000000000000000, 0.000000000000000000, 3.469446951953611033E-15 ) ) ;
#27689=EDGE_LOOP ( 'NONE', ( #5418, #21524 ) ) ;
#27762=DIRECTION ( 'NONE',  ( 0.000000000000000000, 0.000000000000000000, -1.000000000000000000 ) ) ;
#27770=DIRECTION ( 'NONE',  ( 0.000000000000000000, 0.000000000000000000, -1.000000000000000000 ) ) ;
#27783=ORIENTED_EDGE ( 'NONE', *, *, #12048, .T. ) ;
#27848=AXIS2_PLACEMENT_3D ( 'NONE', #24642, #18831, #20150 ) ;
#27885=AXIS2_PLACEMENT_3D ( 'NONE', #3150, #20855, #23218 ) ;
#27918=ORIENTED_EDGE ( 'NONE', *, *, #26984, .T. ) ;
#27938=DIRECTION ( 'NONE',  ( -0.03487826274237476598, -0.9987827659587182882, -0.03487826274237428026 ) ) ;
#27940=SPHERICAL_SURFACE ( 'NONE', #17244, 0.5000000000000000000 ) ;
#27970=FACE_OUTER_BOUND ( 'NONE', #15886, .T. ) ;
#27978=CIRCLE ( 'NONE', #7697, 10.01806974338573752 ) ;
#27993=ORIENTED_EDGE ( 'NONE', *, *, #30405, .F. ) ;
#28037=ORIENTED_EDGE ( 'NONE', *, *, #31259, .T. ) ;
#28063=ORIENTED_EDGE ( 'NONE', *, *, #22164, .F. ) ;
#28083=VERTEX_POINT ( 'NONE', #32222 ) ;
#28120=VERTEX_POINT ( 'NONE', #12127 ) ;
#28121=CARTESIAN_POINT ( 'NONE',  ( -35.00000000000000000, 18.00000000000000355, -0.3702070605508915868 ) ) ;
#28126=FACE_OUTER_BOUND ( 'NONE', #8657, .T. ) ;
#28130=CARTESIAN_POINT ( 'NONE',  ( -34.31843563627105453, 19.51744974835125035, 1.977928362984241017 ) ) ;
#28145=DIRECTION ( 'NONE',  ( 1.000000000000000000, 0.000000000000000000, 1.734723475976805517E-15 ) ) ;
#28147=CARTESIAN_POINT ( 'NONE',  ( 34.71268046341646141, -0.06979899340500209104, -1.021976849372817631 ) ) ;
#28175=EDGE_CURVE ( 'NONE', #8919, #16210, #21536, .T. ) ;
#28189=ADVANCED_FACE ( 'NONE', ( #7428 ), #17469, .T. ) ;
#28220=CARTESIAN_POINT ( 'NONE',  ( 33.81874022276150527, 19.50000000000000000, -1.977928362984232802 ) ) ;
#28234=VERTEX_POINT ( 'NONE', #14946 ) ;
#28236=CARTESIAN_POINT ( 'NONE',  ( -35.00000000000000000, 0.5000000000000000000, -2.482234843104710986 ) ) ;
#28239=DIRECTION ( 'NONE',  ( -0.000000000000000000, -1.000000000000000000, -0.000000000000000000 ) ) ;
#28253=ORIENTED_EDGE ( 'NONE', *, *, #12649, .T. ) ;
#28258=EDGE_CURVE ( 'NONE', #6237, #9415, #16755, .T. ) ;
#28277=FACE_OUTER_BOUND ( 'NONE', #8230, .T. ) ;
#28283=CIRCLE ( 'NONE', #12, 0.5000000000000000000 ) ;
#28316=LINE ( 'NONE', #17804, #17669 ) ;
#28326=ADVANCED_FACE ( 'NONE', ( #768 ), #32796, .T. ) ;
#28333=EDGE_CURVE ( 'NONE', #9245, #773, #28513, .T. ) ;
#28353=AXIS2_PLACEMENT_3D ( 'NONE', #3511, #18534, #23870 ) ;
#28379=AXIS2_PLACEMENT_3D ( 'NONE', #8188, #23061, #487 ) ;
#28388=ADVANCED_FACE ( 'NONE', ( #4420 ), #24803, .T. ) ;
#28389=AXIS2_PLACEMENT_3D ( 'NONE', #28635, #31464, #23774 ) ;
#28401=EDGE_LOOP ( 'NONE', ( #4531, #20817, #6981, #24279 ) ) ;
#28429=DIRECTION ( 'NONE',  ( 0.03487826274237457863, -0.9987827659587181772, 0.03487826274237499496 ) ) ;
#28431=ORIENTED_EDGE ( 'NONE', *, *, #26025, .T. ) ;
#28432=AXIS2_PLACEMENT_3D ( 'NONE', #11909, #4713, #12217 ) ;
#28445=VECTOR ( 'NONE', #4018, 1000.000000000000000 ) ;
#28465=DIRECTION ( 'NONE',  ( -0.03488359650710489562, -0.9989355049964837585, 0.03018263660036206442 ) ) ;
#28466=AXIS2_PLACEMENT_3D ( 'NONE', #28944, #1524, #19425 ) ;
#28492=CIRCLE ( 'NONE', #14046, 0.5000000000000000000 ) ;
#28513=CIRCLE ( 'NONE', #30126, 6.818740222761507042 ) ;
#28552=LINE ( 'NONE', #5794, #12936 ) ;
#28561=EDGE_LOOP ( 'NONE', ( #13096, #14700, #18244, #6596 ) ) ;
#28563=ORIENTED_EDGE ( 'NONE', *, *, #21914, .T. ) ;
#28635=CARTESIAN_POINT ( 'NONE',  ( 0.000000000000000000, 18.00000000000000355, 0.000000000000000000 ) ) ;
#28658=FACE_OUTER_BOUND ( 'NONE', #14219, .T. ) ;
#28677=LINE ( 'NONE', #8592, #29888 ) ;
#28691=EDGE_LOOP ( 'NONE', ( #25762, #13181, #1976, #32037 ) ) ;
#28701=DIRECTION ( 'NONE',  ( 0.7222222222222246524, 0.000000000000000000, -0.6916610887771492688 ) ) ;
#28707=DIRECTION ( 'NONE',  ( -0.000000000000000000, -0.9993908270190956511, -0.03489949670250104552 ) ) ;
#28716=DIRECTION ( 'NONE',  ( 0.7222222222222212107, 1.305870959400644667E-15, -0.6916610887771528215 ) ) ;
#28725=CARTESIAN_POINT ( 'NONE',  ( 12.44989959798878587, 19.50000000000000000, 1.818740222761551451 ) ) ;
#28730=DIRECTION ( 'NONE',  ( -0.1437473352844943209, 0.000000000000000000, 0.9896144216807913896 ) ) ;
#28744=EDGE_CURVE ( 'NONE', #17768, #17909, #7997, .T. ) ;
#28817=CARTESIAN_POINT ( 'NONE',  ( 0.000000000000000000, 20.00000000000000000, 0.000000000000000000 ) ) ;
#28838=LINE ( 'NONE', #13773, #30426 ) ;
#28875=EDGE_LOOP ( 'NONE', ( #6411, #14914, #5797, #5675 ) ) ;
#28909=ORIENTED_EDGE ( 'NONE', *, *, #28258, .F. ) ;
#28914=CARTESIAN_POINT ( 'NONE',  ( 5.772270645472297623, 14.99679128811751916, 2.402751277358659454 ) ) ;
#28927=CIRCLE ( 'NONE', #27327, 0.5000000000000000000 ) ;
#28941=DIRECTION ( 'NONE',  ( -0.000000000000000000, -1.000000000000000000, -0.000000000000000000 ) ) ;
#28944=CARTESIAN_POINT ( 'NONE',  ( -34.48223484310472031, 0.5000000000000000000, -2.482234843104710986 ) ) ;
#28948=CARTESIAN_POINT ( 'NONE',  ( -34.48223484310472031, 0.000000000000000000, -2.482234843104710986 ) ) ;
#28981=VECTOR ( 'NONE', #842, 1000.000000000000000 ) ;
#28987=EDGE_CURVE ( 'NONE', #6030, #3357, #24485, .T. ) ;
#29021=VERTEX_POINT ( 'NONE', #25161 ) ;
#29030=CARTESIAN_POINT ( 'NONE',  ( -34.48223484310472031, 0.5000000000000000000, -2.482234843104710986 ) ) ;
#29069=DIRECTION ( 'NONE',  ( 0.000000000000000000, 0.000000000000000000, -1.000000000000000000 ) ) ;
#29098=VERTEX_POINT ( 'NONE', #17137 ) ;
#29146=CARTESIAN_POINT ( 'NONE',  ( 12.44989959798879831, 18.00000000000000355, 0.3702070605509401036 ) ) ;
#29160=ORIENTED_EDGE ( 'NONE', *, *, #4106, .F. ) ;
#29174=DIRECTION ( 'NONE',  ( -0.9896144216807899463, 0.000000000000000000, -0.1437473352845038410 ) ) ;
#29214=DIRECTION ( 'NONE',  ( 0.000000000000000000, -0.03489949670250130920, -0.9993908270190957621 ) ) ;
#29219=DIRECTION ( 'NONE',  ( 0.000000000000000000, 0.000000000000000000, -1.000000000000000000 ) ) ;
#29223=DIRECTION ( 'NONE',  ( 0.000000000000000000, 1.000000000000000000, 0.000000000000000000 ) ) ;
#29228=ORIENTED_EDGE ( 'NONE', *, *, #5481, .F. ) ;
#29229=EDGE_CURVE ( 'NONE', #29021, #21819, #1054, .T. ) ;
#29283=ORIENTED_EDGE ( 'NONE', *, *, #13463, .T. ) ;
#29305=ORIENTED_EDGE ( 'NONE', *, *, #17371, .F. ) ;
#29321=CARTESIAN_POINT ( 'NONE',  ( 12.44989959798868817, 18.00000000000000355, 13.00000000000004441 ) ) ;
#29330=CIRCLE ( 'NONE', #25592, 0.5000000000000000000 ) ;
#29340=VERTEX_POINT ( 'NONE', #32181 ) ;
#29383=VERTEX_POINT ( 'NONE', #7082 ) ;
#29392=AXIS2_PLACEMENT_3D ( 'NONE', #29404, #19207, #32091 ) ;
#29398=AXIS2_PLACEMENT_3D ( 'NONE', #2399, #23104, #20264 ) ;
#29404=CARTESIAN_POINT ( 'NONE',  ( 34.48223484310469900, 0.5000000000000000000, 2.482234843104950350 ) ) ;
#29432=CARTESIAN_POINT ( 'NONE',  ( 12.44989959798879831, 0.000000000000000000, 0.9987809114024006618 ) ) ;
#29452=VERTEX_POINT ( 'NONE', #20283 ) ;
#29470=ORIENTED_EDGE ( 'NONE', *, *, #24551, .T. ) ;
#29473=AXIS2_PLACEMENT_3D ( 'NONE', #11622, #31537, #8621 ) ;
#29476=ADVANCED_FACE ( 'NONE', ( #18265 ), #10419, .T. ) ;
#29479=CARTESIAN_POINT ( 'NONE',  ( 33.00121834596181714, -0.06979899340500209104, -3.000000000000002665 ) ) ;
#29500=ORIENTED_EDGE ( 'NONE', *, *, #24264, .F. ) ;
#29506=DIRECTION ( 'NONE',  ( 1.000000000000000000, -2.298508605669267507E-14, 1.734723475976805517E-15 ) ) ;
#29511=DIRECTION ( 'NONE',  ( -0.1437473352845045071, 0.000000000000000000, 0.9896144216807898353 ) ) ;
#29528=DIRECTION ( 'NONE',  ( -0.9993908270190957621, 0.03489949670250105246, 0.000000000000000000 ) ) ;
#29578=AXIS2_PLACEMENT_3D ( 'NONE', #22704, #5144, #9822 ) ;
#29590=EDGE_CURVE ( 'NONE', #7057, #27059, #29993, .T. ) ;
#29594=LINE ( 'NONE', #14510, #28445 ) ;
#29611=ORIENTED_EDGE ( 'NONE', *, *, #6497, .F. ) ;
#29623=DIRECTION ( 'NONE',  ( 0.000000000000000000, 1.000000000000000000, 0.000000000000000000 ) ) ;
#29677=EDGE_LOOP ( 'NONE', ( #21488, #32856, #8291, #16556 ) ) ;
#29691=CARTESIAN_POINT ( 'NONE',  ( -5.240875073191923583, 0.000000000000000000, -3.405250132838343102 ) ) ;
#29702=CARTESIAN_POINT ( 'NONE',  ( 34.30400690026458932, 19.51744974835125035, -2.412380016372522196 ) ) ;
#29721=LINE ( 'NONE', #19174, #11293 ) ;
#29749=CARTESIAN_POINT ( 'NONE',  ( -4.716257286563783957, 20.00000000000000000, -4.924645716438867282 ) ) ;
#29752=VERTEX_POINT ( 'NONE', #17515 ) ;
#29781=DIRECTION ( 'NONE',  ( 0.000000000000000000, 0.000000000000000000, 1.000000000000000000 ) ) ;
#29782=SHAPE_REPRESENTATION_RELATIONSHIP ( 'NONE' , 'NONE' ,  #3460, #31139 ) ;
#29785=CARTESIAN_POINT ( 'NONE',  ( -34.55406472725060496, 0.5174497483512505713, 3.046515352619032946 ) ) ;
#29828=CARTESIAN_POINT ( 'NONE',  ( 0.9801757370192293317, 19.50000000000000000, -6.747923662139670320 ) ) ;
#29846=DIRECTION ( 'NONE',  ( -0.9896144216807905014, -0.000000000000000000, -0.1437473352845003161 ) ) ;
#29872=LINE ( 'NONE', #3989, #5560 ) ;
#29888=VECTOR ( 'NONE', #24138, 1000.000000000000114 ) ;
#29927=AXIS2_PLACEMENT_3D ( 'NONE', #19348, #1313, #24003 ) ;
#29947=ORIENTED_EDGE ( 'NONE', *, *, #26933, .T. ) ;
#29952=VERTEX_POINT ( 'NONE', #7436 ) ;
#29957=AXIS2_PLACEMENT_3D ( 'NONE', #25188, #9976, #22351 ) ;
#29973=DIRECTION ( 'NONE',  ( -1.000000000000000000, 0.000000000000000000, -3.469446951953611033E-15 ) ) ;
#29982=ORIENTED_EDGE ( 'NONE', *, *, #8164, .T. ) ;
#29990=AXIS2_PLACEMENT_3D ( 'NONE', #3238, #744, #25474 ) ;
#29993=CIRCLE ( 'NONE', #28389, 3.750000000000000444 ) ;
#29994=AXIS2_PLACEMENT_3D ( 'NONE', #3842, #4015, #32088 ) ;
#29995=VERTEX_POINT ( 'NONE', #12627 ) ;
#29996=CARTESIAN_POINT ( 'NONE',  ( 0.000000000000000000, 0.5174497483512452423, 7.981930256614262476 ) ) ;
#30000=EDGE_LOOP ( 'NONE', ( #1920, #26341, #10380, #5527 ) ) ;
#30010=DIRECTION ( 'NONE',  ( 0.9993908270190957621, -0.03489949670250111491, 0.000000000000000000 ) ) ;
#30013=AXIS2_PLACEMENT_3D ( 'NONE', #23984, #6129, #21506 ) ;
#30038=AXIS2_PLACEMENT_3D ( 'NONE', #12454, #17619, #27661 ) ;
#30055=VERTEX_POINT ( 'NONE', #13274 ) ;
#30057=DIRECTION ( 'NONE',  ( -3.469446951953478110E-15, 0.000000000000000000, 1.000000000000000000 ) ) ;
#30081=CIRCLE ( 'NONE', #32225, 6.250000000000000000 ) ;
#30126=AXIS2_PLACEMENT_3D ( 'NONE', #28817, #8284, #18794 ) ;
#30141=AXIS2_PLACEMENT_3D ( 'NONE', #30384, #32564, #7455 ) ;
#30184=ORIENTED_EDGE ( 'NONE', *, *, #26707, .T. ) ;
#30188=AXIS2_PLACEMENT_3D ( 'NONE', #8570, #16272, #20268 ) ;
#30201=CARTESIAN_POINT ( 'NONE',  ( 34.48223484310472031, 0.5000000000000000000, -2.999999999999997335 ) ) ;
#30219=VERTEX_POINT ( 'NONE', #29996 ) ;
#30222=DIRECTION ( 'NONE',  ( 1.000000000000000000, -0.000000000000000000, 0.000000000000000000 ) ) ;
#30295=ORIENTED_EDGE ( 'NONE', *, *, #18703, .F. ) ;
#30297=LINE ( 'NONE', #22767, #12399 ) ;
#30341=ORIENTED_EDGE ( 'NONE', *, *, #7758, .T. ) ;
#30359=CARTESIAN_POINT ( 'NONE',  ( 33.81874022276149816, 19.50000000000000000, 1.818740222761736192 ) ) ;
#30377=FACE_OUTER_BOUND ( 'NONE', #24548, .T. ) ;
#30384=CARTESIAN_POINT ( 'NONE',  ( 12.44989959798868817, 20.00000000000000000, 13.00000000000004441 ) ) ;
#30405=EDGE_CURVE ( 'NONE', #26914, #23785, #546, .T. ) ;
#30419=CIRCLE ( 'NONE', #535, 0.5000000000000003331 ) ;
#30422=FACE_BOUND ( 'NONE', #27689, .T. ) ;
#30426=VECTOR ( 'NONE', #13452, 1000.000000000000000 ) ;
#30427=CYLINDRICAL_SURFACE ( 'NONE', #23547, 0.5000000000000000000 ) ;
#30448=ORIENTED_EDGE ( 'NONE', *, *, #22165, .F. ) ;
#30498=ORIENTED_EDGE ( 'NONE', *, *, #10837, .F. ) ;
#30515=DIRECTION ( 'NONE',  ( -0.1437473352844943209, 0.000000000000000000, 0.9896144216807913896 ) ) ;
#30548=ORIENTED_EDGE ( 'NONE', *, *, #32827, .T. ) ;
#30574=CIRCLE ( 'NONE', #25758, 6.250000000000000000 ) ;
#30611=ORIENTED_EDGE ( 'NONE', *, *, #5908, .F. ) ;
#30630=DIRECTION ( 'NONE',  ( -0.1436597682917712671, 0.03489949670250103858, 0.9890115753135888532 ) ) ;
#30632=AXIS2_PLACEMENT_3D ( 'NONE', #6529, #8716, #16544 ) ;
#30660=EDGE_CURVE ( 'NONE', #6030, #11692, #24926, .T. ) ;
#30670=CARTESIAN_POINT ( 'NONE',  ( 34.48223484310466347, 0.000000000000000000, 13.00000000000012079 ) ) ;
#30701=CARTESIAN_POINT ( 'NONE',  ( -34.48223484310472031, 0.5000000000000000000, 2.552009564962238297 ) ) ;
#30758=ADVANCED_FACE ( 'NONE', ( #19442 ), #2039, .T. ) ;
#30759=CARTESIAN_POINT ( 'NONE',  ( 34.98223484310472031, 0.5000000000000000000, -2.552009564962228527 ) ) ;
#30777=DIRECTION ( 'NONE',  ( 2.637475533091417728E-15, 0.000000000000000000, 1.000000000000000000 ) ) ;
#30791=CARTESIAN_POINT ( 'NONE',  ( -32.99878091140236336, 0.000000000000000000, 3.000000000000004441 ) ) ;
#30805=VERTEX_POINT ( 'NONE', #11368 ) ;
#30808=PLANE ( 'NONE',  #17753 ) ;
#30820=ADVANCED_FACE ( 'NONE', ( #23745 ), #7078, .T. ) ;
#30825=CARTESIAN_POINT ( 'NONE',  ( -33.81874022276151237, 20.00000000000000000, 2.395703997917905337 ) ) ;
#30838=DIRECTION ( 'NONE',  ( 0.9993908270190957621, 0.03489949670250118430, 0.000000000000000000 ) ) ;
#30850=ORIENTED_EDGE ( 'NONE', *, *, #25118, .T. ) ;
#30890=ORIENTED_EDGE ( 'NONE', *, *, #1096, .F. ) ;
#30893=DIRECTION ( 'NONE',  ( 0.000000000000000000, -0.9993908270190956511, 0.03489949670250104552 ) ) ;
#30898=DIRECTION ( 'NONE',  ( -0.6916610887771488247, 0.000000000000000000, -0.7222222222222250965 ) ) ;
#30913=EDGE_CURVE ( 'NONE', #5967, #8298, #25664, .T. ) ;
#30932=EDGE_CURVE ( 'NONE', #72, #28120, #29594, .T. ) ;
#30937=CARTESIAN_POINT ( 'NONE',  ( 5.061877160328730696, 19.51744974835124680, 5.285536848417998534 ) ) ;
#30989=EDGE_LOOP ( 'NONE', ( #21571, #31700, #7369, #2787, #32915 ) ) ;
#30992=CARTESIAN_POINT ( 'NONE',  ( 13.06177556439308418, 19.50000000000000000, 8.787599961869133836 ) ) ;
#31019=CIRCLE ( 'NONE', #16572, 0.5000000000000004441 ) ;
#31030=ORIENTED_EDGE ( 'NONE', *, *, #5897, .F. ) ;
#31044=CARTESIAN_POINT ( 'NONE',  ( -5.175170698068149555, 0.5000000000000000000, -5.403836275575627290 ) ) ;
#31056=CARTESIAN_POINT ( 'NONE',  ( 0.000000000000000000, 37.67766952966368876, 0.000000000000000000 ) ) ;
#31067=AXIS2_PLACEMENT_3D ( 'NONE', #9275, #21501, #31714 ) ;
#31085=DIRECTION ( 'NONE',  ( 0.9896144216807900573, 0.000000000000000000, 0.1437473352845035912 ) ) ;
#31120=AXIS2_PLACEMENT_3D ( 'NONE', #9890, #19751, #4061 ) ;
#31132=DIRECTION ( 'NONE',  ( -0.000000000000000000, -1.000000000000000000, -0.000000000000000000 ) ) ;
#31136=ORIENTED_EDGE ( 'NONE', *, *, #14012, .F. ) ;
#31138=CARTESIAN_POINT ( 'NONE',  ( 0.000000000000000000, 19.50000000000000000, 6.818740222761507042 ) ) ;
#31139=ADVANCED_BREP_SHAPE_REPRESENTATION ( '', ( #32572, #2865 ), #7102 ) ;
#31147=AXIS2_PLACEMENT_3D ( 'NONE', #25964, #5393, #7561 ) ;
#31153=LINE ( 'NONE', #8238, #9197 ) ;
#31155=DIRECTION ( 'NONE',  ( -0.000000000000000000, -0.000000000000000000, 1.000000000000000000 ) ) ;
#31157=CARTESIAN_POINT ( 'NONE',  ( 12.44989959798878232, 0.4999999999999998890, 2.482234843104758060 ) ) ;
#31178=AXIS2_PLACEMENT_3D ( 'NONE', #1512, #31943, #9008 ) ;
#31179=DIRECTION ( 'NONE',  ( -0.9896144216807899463, 0.000000000000000000, -0.1437473352845038410 ) ) ;
#31236=DIRECTION ( 'NONE',  ( 0.000000000000000000, 0.000000000000000000, -1.000000000000000000 ) ) ;
#31259=EDGE_CURVE ( 'NONE', #14980, #15111, #11376, .T. ) ;
#31274=ADVANCED_FACE ( 'NONE', ( #3758 ), #11453, .F. ) ;
#31300=DIRECTION ( 'NONE',  ( 0.9993908270190957621, 0.03489949670250133695, 0.000000000000000000 ) ) ;
#31321=LINE ( 'NONE', #15771, #5921 ) ;
#31337=CARTESIAN_POINT ( 'NONE',  ( 12.44989959798877699, 0.5000000000000000000, 2.982234843104758060 ) ) ;
#31389=CARTESIAN_POINT ( 'NONE',  ( -12.44989959798873791, -0.06979899340500209104, -1.001218345961804257 ) ) ;
#31420=EDGE_CURVE ( 'NONE', #22752, #20668, #17300, .T. ) ;
#31441=EDGE_LOOP ( 'NONE', ( #2275, #25558, #16129, #29982, #9737 ) ) ;
#31460=ADVANCED_FACE ( 'NONE', ( #20144 ), #15779, .F. ) ;
#31464=DIRECTION ( 'NONE',  ( 0.000000000000000000, 1.000000000000000000, 0.000000000000000000 ) ) ;
#31493=EDGE_LOOP ( 'NONE', ( #32352, #10881, #4899, #24554, #4990 ) ) ;
#31513=ADVANCED_FACE ( 'NONE', ( #25633 ), #2748, .T. ) ;
#31531=CARTESIAN_POINT ( 'NONE',  ( 32.99878091140236336, 0.000000000000000000, -3.000000000000002665 ) ) ;
#31537=DIRECTION ( 'NONE',  ( 0.000000000000000000, 1.000000000000000000, 0.000000000000000000 ) ) ;
#31546=FACE_OUTER_BOUND ( 'NONE', #23515, .T. ) ;
#31557=AXIS2_PLACEMENT_3D ( 'NONE', #10507, #2508, #12343 ) ;
#31576=VECTOR ( 'NONE', #31870, 1000.000000000000000 ) ;
#31611=AXIS2_PLACEMENT_3D ( 'NONE', #16717, #3381, #21098 ) ;
#31622=EDGE_CURVE ( 'NONE', #22141, #16462, #2868, .T. ) ;
#31670=AXIS2_PLACEMENT_3D ( 'NONE', #2890, #12705, #13055 ) ;
#31679=CARTESIAN_POINT ( 'NONE',  ( 33.81874022276151237, 20.00000000000000000, -1.977928362984232802 ) ) ;
#31693=EDGE_LOOP ( 'NONE', ( #30448, #27918, #8257, #18555, #6786 ) ) ;
#31700=ORIENTED_EDGE ( 'NONE', *, *, #23362, .T. ) ;
#31712=AXIS2_PLACEMENT_3D ( 'NONE', #3729, #26624, #1401 ) ;
#31714=DIRECTION ( 'NONE',  ( 0.000000000000000000, 0.000000000000000000, -1.000000000000000000 ) ) ;
#31742=EDGE_LOOP ( 'NONE', ( #20228, #21378, #21155, #27479 ) ) ;
#31749=ORIENTED_EDGE ( 'NONE', *, *, #15175, .F. ) ;
#31771=ORIENTED_EDGE ( 'NONE', *, *, #8828, .F. ) ;
#31790=CARTESIAN_POINT ( 'NONE',  ( -5.175170698068149555, 0.5000000000000000000, -5.403836275575627290 ) ) ;
#31813=ORIENTED_EDGE ( 'NONE', *, *, #15628, .T. ) ;
#31821=EDGE_CURVE ( 'NONE', #24347, #24965, #1186, .T. ) ;
#31855=CARTESIAN_POINT ( 'NONE',  ( 34.48223484310469900, 0.5000000000000000000, 2.482234843104950350 ) ) ;
#31863=DIRECTION ( 'NONE',  ( -0.6916610887771522664, 0.000000000000000000, -0.7222222222222217658 ) ) ;
#31870=DIRECTION ( 'NONE',  ( 3.469446951953478110E-15, -0.000000000000000000, -1.000000000000000000 ) ) ;
#31897=CARTESIAN_POINT ( 'NONE',  ( 0.000000000000000000, 20.00000000000000000, 0.000000000000000000 ) ) ;
#31900=ORIENTED_EDGE ( 'NONE', *, *, #27593, .F. ) ;
#31943=DIRECTION ( 'NONE',  ( 1.000000000000000000, -0.000000000000000000, 0.000000000000000000 ) ) ;
#31950=DIRECTION ( 'NONE',  ( 0.000000000000000000, 1.000000000000000000, 0.000000000000000000 ) ) ;
#31990=DIRECTION ( 'NONE',  ( 1.000000000000000000, 0.000000000000000000, 3.469446951953611033E-15 ) ) ;
#32009=DIRECTION ( 'NONE',  ( 0.000000000000000000, 0.000000000000000000, 1.000000000000000000 ) ) ;
#32016=PLANE ( 'NONE',  #22476 ) ;
#32024=CARTESIAN_POINT ( 'NONE',  ( 3.526383166312418993, 10.27186380921758335, -5.187041768249670781 ) ) ;
#32027=DIRECTION ( 'NONE',  ( 0.000000000000000000, 1.000000000000000000, 0.000000000000000000 ) ) ;
#32037=ORIENTED_EDGE ( 'NONE', *, *, #23362, .F. ) ;
#32088=DIRECTION ( 'NONE',  ( 0.000000000000000000, 0.000000000000000000, 1.000000000000000000 ) ) ;
#32091=DIRECTION ( 'NONE',  ( 1.387778780781445676E-14, 0.000000000000000000, -1.000000000000000000 ) ) ;
#32103=VECTOR ( 'NONE', #6771, 1000.000000000000227 ) ;
#32110=CIRCLE ( 'NONE', #28379, 10.68156436372894902 ) ;
#32124=DIRECTION ( 'NONE',  ( -1.000000000000000000, 0.000000000000000000, 0.000000000000000000 ) ) ;
#32138=EDGE_LOOP ( 'NONE', ( #5545, #3589, #20099, #14407, #20025 ) ) ;
#32156=EDGE_CURVE ( 'NONE', #32786, #15111, #4545, .T. ) ;
#32181=CARTESIAN_POINT ( 'NONE',  ( -5.175170698068149555, 0.000000000000000000, -5.403836275575627290 ) ) ;
#32203=VECTOR ( 'NONE', #12067, 1000.000000000000227 ) ;
#32207=ADVANCED_FACE ( 'NONE', ( #22252 ), #16894, .T. ) ;
#32209=TOROIDAL_SURFACE ( 'NONE', #14010, 7.482234843104714983, 0.5000000000000000000 ) ;
#32222=CARTESIAN_POINT ( 'NONE',  ( -34.98193025661426248, 0.5174497483512505713, 2.552009564962238297 ) ) ;
#32225=AXIS2_PLACEMENT_3D ( 'NONE', #32884, #20165, #15297 ) ;
#32229=ORIENTED_EDGE ( 'NONE', *, *, #6195, .T. ) ;
#32275=ADVANCED_FACE ( 'NONE', ( #24569 ), #11318, .T. ) ;
#32339=FACE_OUTER_BOUND ( 'NONE', #12620, .T. ) ;
#32352=ORIENTED_EDGE ( 'NONE', *, *, #15986, .T. ) ;
#32367=CARTESIAN_POINT ( 'NONE',  ( 34.48223484310469900, 0.000000000000000000, 2.482234843104950350 ) ) ;
#32373=ADVANCED_FACE ( 'NONE', ( #20412 ), #15221, .T. ) ;
#32407=CARTESIAN_POINT ( 'NONE',  ( 34.99999999999998579, 0.000000000000000000, 3.000000000000239364 ) ) ;
#32461=VERTEX_POINT ( 'NONE', #9878 ) ;
#32474=ORIENTED_EDGE ( 'NONE', *, *, #4547, .T. ) ;
#32496=LINE ( 'NONE', #5076, #13992 ) ;
#32497=CYLINDRICAL_SURFACE ( 'NONE', #9164, 0.5000000000000002220 ) ;
#32500=ADVANCED_FACE ( 'NONE', ( #6175 ), #8015, .T. ) ;
#32510=ORIENTED_EDGE ( 'NONE', *, *, #22335, .T. ) ;
#32527=DIRECTION ( 'NONE',  ( 0.1437473352844943209, 0.000000000000000000, -0.9896144216807913896 ) ) ;
#32547=DIRECTION ( 'NONE',  ( -1.000000000000000000, 0.000000000000000000, -8.654346879536960414E-15 ) ) ;
#32564=DIRECTION ( 'NONE',  ( 0.000000000000000000, 1.000000000000000000, 0.000000000000000000 ) ) ;
#32572=MANIFOLD_SOLID_BREP ( 'Fillet1', #7073 ) ;
#32588=AXIS2_PLACEMENT_3D ( 'NONE', #8649, #18870, #29069 ) ;
#32598=CIRCLE ( 'NONE', #10164, 12.00121908859764552 ) ;
#32605=ORIENTED_EDGE ( 'NONE', *, *, #9421, .F. ) ;
#32616=DIRECTION ( 'NONE',  ( -0.000000000000000000, 0.000000000000000000, -1.000000000000000000 ) ) ;
#32628=ORIENTED_EDGE ( 'NONE', *, *, #24325, .T. ) ;
#32672=EDGE_LOOP ( 'NONE', ( #31771, #14345, #1901, #860 ) ) ;
#32696=AXIS2_PLACEMENT_3D ( 'NONE', #19448, #24777, #27762 ) ;
#32732=LINE ( 'NONE', #20028, #2207 ) ;
#32770=AXIS2_PLACEMENT_3D ( 'NONE', #21099, #21247, #11049 ) ;
#32786=VERTEX_POINT ( 'NONE', #30759 ) ;
#32791=CIRCLE ( 'NONE', #1834, 0.5000000000000000000 ) ;
#32796=TOROIDAL_SURFACE ( 'NONE', #13014, 10.51776515689528502, 0.5000000000000000000 ) ;
#32827=EDGE_CURVE ( 'NONE', #9415, #9377, #22718, .T. ) ;
#32856=ORIENTED_EDGE ( 'NONE', *, *, #9846, .T. ) ;
#32876=FACE_OUTER_BOUND ( 'NONE', #14910, .T. ) ;
#32884=CARTESIAN_POINT ( 'NONE',  ( 0.000000000000000000, 18.00000000000000355, 0.000000000000000000 ) ) ;
#32912=LINE ( 'NONE', #22710, #8659 ) ;
#32915=ORIENTED_EDGE ( 'NONE', *, *, #82, .F. ) ;
#32916=ADVANCED_FACE ( 'NONE', ( #25894 ), #10495, .T. ) ;
#32923=CARTESIAN_POINT ( 'NONE',  ( 12.44989959798878232, 19.51744974835125035, 2.318435636271098943 ) ) ;
#32929=ADVANCED_FACE ( 'NONE', ( #31546 ), #9182, .T. ) ;
#32944=FACE_BOUND ( 'NONE', #31441, .T. ) ;
#32959=ORIENTED_EDGE ( 'NONE', *, *, #12814, .T. ) ;
#32963=ORIENTED_EDGE ( 'NONE', *, *, #25482, .T. ) ;
#32974=DIRECTION ( 'NONE',  ( 0.9896144216807899463, -0.000000000000000000, 0.1437473352845035635 ) ) ;
#33013=DIRECTION ( 'NONE',  ( -1.000000000000000000, 0.000000000000000000, 0.000000000000000000 ) ) ;
#33058=DIRECTION ( 'NONE',  ( 1.000000000000000000, 0.000000000000000000, 0.000000000000000000 ) ) ;
#33071=EDGE_CURVE ( 'NONE', #5967, #28234, #30081, .T. ) ;
#33113=COLOUR_RGB('Light Blue', 0.31764706, 0.68627451, 0.89019608);
#33114=FILL_AREA_STYLE_COLOUR('',#33113);
#33115=FILL_AREA_STYLE('',(#33114));
#33116=SURFACE_STYLE_FILL_AREA(#33115);
#33117=SURFACE_SIDE_STYLE('',(#33116));
#33118=SURFACE_STYLE_USAGE(.BOTH.,#33117);
#33119=PRESENTATION_STYLE_ASSIGNMENT((#33118));
#33162=STYLED_ITEM('',(#33119),#32572);
#33163=MECHANICAL_DESIGN_GEOMETRIC_PRESENTATION_REPRESENTATION('',(#33162),#7102);
ENDSEC;
END-ISO-10303-21;
